ISO-10303-21;
HEADER;
FILE_DESCRIPTION (('STEP AP214'),
    '1' );
FILE_NAME ('Shackle.step',
    '2026-10-06T10:59:17',
    ( '' ),
    ( '' ),
    'SwSTEP 2.0',
    'SolidWorks 2026',
    '' );
FILE_SCHEMA (( 'AUTOMOTIVE_DESIGN' ));
ENDSEC;

DATA;
#39=CARTESIAN_POINT ( 'NONE',  ( -1.214884381343047881, 47.76843358786783966, 61.41730067788144964 ) ) ;
#44=ORIENTED_EDGE ( 'NONE', *, *, #9004, .T. ) ;
#67=CARTESIAN_POINT ( 'NONE',  ( 2.522153740306511072, 49.16218137147969003, 50.55433879953100273 ) ) ;
#77=CARTESIAN_POINT ( 'NONE',  ( 2.122153740306496505, 47.82824192744437397, 69.55433879953100984 ) ) ;
#80=CARTESIAN_POINT ( 'NONE',  ( 0.5221537403065104055, 40.36218137147969998, 46.15433879953098284 ) ) ;
#89=ORIENTED_EDGE ( 'NONE', *, *, #15661, .F. ) ;
#98=CARTESIAN_POINT ( 'NONE',  ( 32.52215374030649286, 44.16218137147969003, 105.5543387995310098 ) ) ;
#109=CARTESIAN_POINT ( 'NONE',  ( -1.477846259693489150, 50.16218137147969713, 53.15433879953100416 ) ) ;
#118=ADVANCED_FACE ( 'NONE', ( #19767 ), #15314, .F. ) ;
#130=AXIS2_PLACEMENT_3D ( 'NONE', #14597, #8214, #5004 ) ;
#131=CARTESIAN_POINT ( 'NONE',  ( -1.477846259693492481, 49.81903562097207327, 69.15433879953098995 ) ) ;
#140=VERTEX_POINT ( 'NONE', #614 ) ;
#145=ADVANCED_FACE ( 'NONE', ( #13399 ), #7094, .T. ) ;
#161=DIRECTION ( 'NONE',  ( -1.779391786395883536E-16, -5.922860397471806844E-17, 1.000000000000000000 ) ) ;
#170=DIRECTION ( 'NONE',  ( -4.731737692062685363E-17, 0.7071067811865536790, 0.7071067811865414665 ) ) ;
#190=EDGE_LOOP ( 'NONE', ( #6563, #851, #9237, #15797, #220 ) ) ;
#196=DIRECTION ( 'NONE',  ( 0.000000000000000000, 1.000000000000000000, 0.000000000000000000 ) ) ;
#209=SHAPE_REPRESENTATION ( 'Shackle', ( #18366 ), #4082 ) ;
#219=EDGE_CURVE ( 'NONE', #16835, #11136, #4609, .T. ) ;
#220=ORIENTED_EDGE ( 'NONE', *, *, #14561, .T. ) ;
#228=AXIS2_PLACEMENT_3D ( 'NONE', #7472, #20221, #2262 ) ;
#243=CARTESIAN_POINT ( 'NONE',  ( 2.522153740306509295, 47.62628298661744708, 61.15433879953099705 ) ) ;
#248=DIRECTION ( 'NONE',  ( 1.000000000000000000, -1.110223024625156540E-16, 1.779391786395883043E-16 ) ) ;
#256=DIRECTION ( 'NONE',  ( -1.000000000000000000, 0.000000000000000000, 0.000000000000000000 ) ) ;
#258=CARTESIAN_POINT ( 'NONE',  ( -1.477846259693481601, 49.81903562097206617, 123.5543387995310098 ) ) ;
#276=DIRECTION ( 'NONE',  ( -1.110223024625156540E-16, -1.000000000000000000, -5.922860397471808077E-17 ) ) ;
#278=FACE_OUTER_BOUND ( 'NONE', #7758, .T. ) ;
#331=ORIENTED_EDGE ( 'NONE', *, *, #15896, .T. ) ;
#337=CARTESIAN_POINT ( 'NONE',  ( 0.5221537403065064087, 48.16218137147969003, 82.55433879953099563 ) ) ;
#338=EDGE_LOOP ( 'NONE', ( #4433, #13539, #17360, #8721, #20536, #4730 ) ) ;
#344=ORIENTED_EDGE ( 'NONE', *, *, #19982, .T. ) ;
#347=VERTEX_POINT ( 'NONE', #243 ) ;
#349=LINE ( 'NONE', #9955, #14871 ) ;
#379=CARTESIAN_POINT ( 'NONE',  ( 2.122153740306508496, 50.16218137147969713, 77.55433879953099563 ) ) ;
#380=ADVANCED_FACE ( 'NONE', ( #1859 ), #12576, .T. ) ;
#384=FACE_OUTER_BOUND ( 'NONE', #4989, .T. ) ;
#390=DIRECTION ( 'NONE',  ( -2.267473790562806355E-16, 5.922860397471811774E-17, -1.000000000000000000 ) ) ;
#399=ORIENTED_EDGE ( 'NONE', *, *, #5094, .F. ) ;
#451=CARTESIAN_POINT ( 'NONE',  ( 0.5221537403065064087, 48.16218137147969003, 50.55433879953100273 ) ) ;
#462=CARTESIAN_POINT ( 'NONE',  ( 2.122153740306511160, 47.82824192744436687, 61.55433879953100273 ) ) ;
#500=VERTEX_POINT ( 'NONE', #77 ) ;
#517=CARTESIAN_POINT ( 'NONE',  ( -1.477846259693498476, 49.81903562097206617, 67.21119304902336467 ) ) ;
#528=CARTESIAN_POINT ( 'NONE',  ( 28.52215374030649642, 44.16218137147969003, 105.5543387995310098 ) ) ;
#535=CARTESIAN_POINT ( 'NONE',  ( -1.077846259693481024, 50.16218137147969713, 69.55433879953100984 ) ) ;
#550=DIRECTION ( 'NONE',  ( -0.5773502691896219563, 0.5773502691896226224, -0.5773502691896327255 ) ) ;
#584=CIRCLE ( 'NONE', #4658, 3.999999999999996447 ) ;
#594=ORIENTED_EDGE ( 'NONE', *, *, #1429, .T. ) ;
#596=AXIS2_PLACEMENT_3D ( 'NONE', #2312, #15191, #5384 ) ;
#605=ORIENTED_EDGE ( 'NONE', *, *, #8324, .F. ) ;
#614=CARTESIAN_POINT ( 'NONE',  ( 2.522153740306493308, 49.81903562097208749, 59.21119304902340019 ) ) ;
#618=VERTEX_POINT ( 'NONE', #18367 ) ;
#630=EDGE_CURVE ( 'NONE', #9317, #1035, #3784, .T. ) ;
#632=ORIENTED_EDGE ( 'NONE', *, *, #10851, .F. ) ;
#642=CARTESIAN_POINT ( 'NONE',  ( 28.52215374030649642, 40.16218137147968292, 87.85433879953103542 ) ) ;
#644=ADVANCED_FACE ( 'NONE', ( #384 ), #18159, .T. ) ;
#653=DIRECTION ( 'NONE',  ( 1.110223024625156540E-16, 1.000000000000000000, 5.922860397471808077E-17 ) ) ;
#659=ORIENTED_EDGE ( 'NONE', *, *, #9004, .F. ) ;
#662=AXIS2_PLACEMENT_3D ( 'NONE', #12850, #6249, #17746 ) ;
#665=PLANE ( 'NONE',  #18587 ) ;
#667=VERTEX_POINT ( 'NONE', #6965 ) ;
#696=ORIENTED_EDGE ( 'NONE', *, *, #11737, .F. ) ;
#709=ORIENTED_EDGE ( 'NONE', *, *, #18588, .F. ) ;
#712=FACE_OUTER_BOUND ( 'NONE', #19202, .T. ) ;
#735=CARTESIAN_POINT ( 'NONE',  ( 2.522153740306494196, 49.81903562097208749, 67.21119304902339309 ) ) ;
#739=CARTESIAN_POINT ( 'NONE',  ( 28.52215374030650352, 44.16218137147969003, 105.5543387995309956 ) ) ;
#747=FACE_OUTER_BOUND ( 'NONE', #12608, .T. ) ;
#754=FACE_OUTER_BOUND ( 'NONE', #10086, .T. ) ;
#758=CIRCLE ( 'NONE', #14682, 4.000000000000000000 ) ;
#761=VECTOR ( 'NONE', #8337, 1000.000000000000000 ) ;
#762=CARTESIAN_POINT ( 'NONE',  ( 2.522153740306507963, 49.16218137147969003, 66.55433879953099563 ) ) ;
#771=CARTESIAN_POINT ( 'NONE',  ( 1.215246153217547365, 50.28109722957945849, 59.67325465763076409 ) ) ;
#775=CARTESIAN_POINT ( 'NONE',  ( 0.5221537403065364957, 44.16218137147969003, 123.5543387995310098 ) ) ;
#786=DIRECTION ( 'NONE',  ( 0.7071067811865539010, -3.662367542345418158E-17, -0.7071067811865411334 ) ) ;
#802=ADVANCED_FACE ( 'NONE', ( #9845 ), #1442, .T. ) ;
#806=ORIENTED_EDGE ( 'NONE', *, *, #4198, .F. ) ;
#807=DIRECTION ( 'NONE',  ( 2.043266227890062685E-16, 0.7071067811865451302, -0.7071067811865500152 ) ) ;
#809=ADVANCED_FACE ( 'NONE', ( #8244 ), #7929, .T. ) ;
#810=EDGE_CURVE ( 'NONE', #4828, #14664, #20355, .T. ) ;
#824=ORIENTED_EDGE ( 'NONE', *, *, #3471, .T. ) ;
#831=EDGE_CURVE ( 'NONE', #13896, #1135, #9541, .T. ) ;
#842=CARTESIAN_POINT ( 'NONE',  ( -0.1709386726045625804, 50.28109722957944427, 67.67325465763074988 ) ) ;
#843=DIRECTION ( 'NONE',  ( -9.598494438985367424E-18, 5.922860397471809309E-17, -1.000000000000000000 ) ) ;
#847=LINE ( 'NONE', #20417, #14344 ) ;
#851=ORIENTED_EDGE ( 'NONE', *, *, #831, .F. ) ;
#864=CARTESIAN_POINT ( 'NONE',  ( 0.5221537403065118488, 48.16218137147969003, 45.55433879953100273 ) ) ;
#877=FACE_OUTER_BOUND ( 'NONE', #6596, .T. ) ;
#880=VERTEX_POINT ( 'NONE', #9961 ) ;
#881=CARTESIAN_POINT ( 'NONE',  ( -3.477846259693496478, 44.16218137147969003, 105.5543387995310098 ) ) ;
#927=ORIENTED_EDGE ( 'NONE', *, *, #5864, .F. ) ;
#961=PLANE ( 'NONE',  #7240 ) ;
#983=VERTEX_POINT ( 'NONE', #9062 ) ;
#1011=CARTESIAN_POINT ( 'NONE',  ( 29.77115333998618496, 40.36218137147969287, 87.85433879953102121 ) ) ;
#1015=VERTEX_POINT ( 'NONE', #4043 ) ;
#1024=EDGE_CURVE ( 'NONE', #5759, #15353, #8350, .T. ) ;
#1035=VERTEX_POINT ( 'NONE', #2234 ) ;
#1042=EDGE_CURVE ( 'NONE', #1280, #4828, #6424, .T. ) ;
#1052=CARTESIAN_POINT ( 'NONE',  ( 24.52215374030650352, 44.16218137147969003, 105.5543387995309956 ) ) ;
#1074=VECTOR ( 'NONE', #13384, 1000.000000000000000 ) ;
#1102=LINE ( 'NONE', #14466, #8401 ) ;
#1135=VERTEX_POINT ( 'NONE', #5409 ) ;
#1180=FACE_OUTER_BOUND ( 'NONE', #5813, .T. ) ;
#1185=CARTESIAN_POINT ( 'NONE',  ( 0.5221537403065061866, 44.16218137147969713, 74.55433879953100984 ) ) ;
#1211=VERTEX_POINT ( 'NONE', #10668 ) ;
#1252=FACE_OUTER_BOUND ( 'NONE', #18310, .T. ) ;
#1268=VERTEX_POINT ( 'NONE', #67 ) ;
#1272=CARTESIAN_POINT ( 'NONE',  ( -1.077846259693497899, 47.82824192744436687, 85.55433879953100984 ) ) ;
#1275=EDGE_CURVE ( 'NONE', #7517, #13896, #11465, .T. ) ;
#1277=FACE_OUTER_BOUND ( 'NONE', #14353, .T. ) ;
#1280=VERTEX_POINT ( 'NONE', #16349 ) ;
#1282=CIRCLE ( 'NONE', #5337, 4.000000000000003553 ) ;
#1345=CARTESIAN_POINT ( 'NONE',  ( 0.5221537403065067418, 50.16218137147969713, 75.55433879953099563 ) ) ;
#1349=LINE ( 'NONE', #3045, #6807 ) ;
#1353=DIRECTION ( 'NONE',  ( 1.779391786395883536E-16, 5.922860397471806844E-17, -1.000000000000000000 ) ) ;
#1363=PLANE ( 'NONE',  #17340 ) ;
#1378=CARTESIAN_POINT ( 'NONE',  ( 2.522153740306505298, 50.16218137147969713, 85.55433879953100984 ) ) ;
#1391=ADVANCED_FACE ( 'NONE', ( #7503 ), #13879, .F. ) ;
#1397=CARTESIAN_POINT ( 'NONE',  ( -1.077846259693493458, 49.76218137147969856, 61.55433879953100273 ) ) ;
#1403=( BOUNDED_CURVE ( )  B_SPLINE_CURVE ( 3, ( #735, #6999, #842, #517 ),
 .UNSPECIFIED., .F., .F. ) 
 B_SPLINE_CURVE_WITH_KNOTS ( ( 4, 4 ),
 ( 2.801755744135677073, 3.481429563043919373 ),
 .UNSPECIFIED. ) 
 CURVE ( )  GEOMETRIC_REPRESENTATION_ITEM ( )  RATIONAL_B_SPLINE_CURVE ( ( 1.000000000000000000, 0.9618726943880423486, 0.9618726943880423486, 1.000000000000000000 ) ) 
 REPRESENTATION_ITEM ( '' )  );
#1404=LINE ( 'NONE', #7587, #4734 ) ;
#1411=CARTESIAN_POINT ( 'NONE',  ( -1.477846259693495146, 50.16218137147969713, 82.55433879953099563 ) ) ;
#1415=ORIENTED_EDGE ( 'NONE', *, *, #10439, .F. ) ;
#1416=FACE_OUTER_BOUND ( 'NONE', #13377, .T. ) ;
#1419=EDGE_CURVE ( 'NONE', #19018, #15529, #2286, .T. ) ;
#1421=DIRECTION ( 'NONE',  ( 1.110223024625156540E-16, 1.000000000000000000, 5.922860397471808077E-17 ) ) ;
#1429=EDGE_CURVE ( 'NONE', #983, #18875, #11987, .T. ) ;
#1435=EDGE_LOOP ( 'NONE', ( #18300, #20002 ) ) ;
#1442=CYLINDRICAL_SURFACE ( 'NONE', #4857, 4.000000000000000000 ) ;
#1449=VECTOR ( 'NONE', #2857, 1000.000000000000114 ) ;
#1470=LINE ( 'NONE', #1675, #17236 ) ;
#1473=AXIS2_PLACEMENT_3D ( 'NONE', #739, #6909, #5527 ) ;
#1474=DIRECTION ( 'NONE',  ( 1.110223024625156540E-16, 1.000000000000000000, 5.922860397471808077E-17 ) ) ;
#1485=CIRCLE ( 'NONE', #20502, 3.999999999999996447 ) ;
#1505=CARTESIAN_POINT ( 'NONE',  ( 28.09439724277525130, 40.36218137147969287, 87.65433879953101837 ) ) ;
#1511=LINE ( 'NONE', #17881, #7558 ) ;
#1514=ORIENTED_EDGE ( 'NONE', *, *, #5438, .F. ) ;
#1524=ORIENTED_EDGE ( 'NONE', *, *, #12510, .T. ) ;
#1527=CARTESIAN_POINT ( 'NONE',  ( 1.119863296874942682, 50.25084051303457500, 77.06567965797613340 ) ) ;
#1541=LINE ( 'NONE', #16121, #19270 ) ;
#1565=ORIENTED_EDGE ( 'NONE', *, *, #18553, .F. ) ;
#1576=EDGE_CURVE ( 'NONE', #5980, #14474, #15264, .T. ) ;
#1584=DIRECTION ( 'NONE',  ( 0.7071067811865479058, -3.662367542345315236E-17, -0.7071067811865472397 ) ) ;
#1589=ORIENTED_EDGE ( 'NONE', *, *, #16507, .T. ) ;
#1629=CARTESIAN_POINT ( 'NONE',  ( -1.477846259693495590, 49.16218137147968292, 82.55433879953099563 ) ) ;
#1630=DIRECTION ( 'NONE',  ( 1.000000000000000000, -1.110223024625156171E-16, -4.142850521348544074E-16 ) ) ;
#1640=VERTEX_POINT ( 'NONE', #11536 ) ;
#1657=EDGE_CURVE ( 'NONE', #18483, #13663, #4708, .T. ) ;
#1668=ORIENTED_EDGE ( 'NONE', *, *, #16638, .T. ) ;
#1669=CARTESIAN_POINT ( 'NONE',  ( -1.477846259693492925, 49.16218137147969003, 66.55433879953099563 ) ) ;
#1675=CARTESIAN_POINT ( 'NONE',  ( -1.077846259693497677, 50.16218137147969713, 85.55433879953100984 ) ) ;
#1695=CIRCLE ( 'NONE', #16298, 3.999999999999996447 ) ;
#1698=AXIS2_PLACEMENT_3D ( 'NONE', #13134, #14414, #12927 ) ;
#1699=CARTESIAN_POINT ( 'NONE',  ( -1.077846259693492348, 47.82824192744436687, 53.55433879953100273 ) ) ;
#1700=DIRECTION ( 'NONE',  ( -1.000000000000000000, 1.110223024625156540E-16, -1.779391786395883043E-16 ) ) ;
#1729=ORIENTED_EDGE ( 'NONE', *, *, #17649, .T. ) ;
#1744=DIRECTION ( 'NONE',  ( 4.142850521348544074E-16, -5.922860397471813007E-17, 1.000000000000000000 ) ) ;
#1761=VECTOR ( 'NONE', #5116, 1000.000000000000114 ) ;
#1763=AXIS2_PLACEMENT_3D ( 'NONE', #4022, #5522, #19976 ) ;
#1789=DIRECTION ( 'NONE',  ( 1.779391786395883536E-16, 5.922860397471806844E-17, -1.000000000000000000 ) ) ;
#1796=VECTOR ( 'NONE', #12356, 999.9999999999998863 ) ;
#1822=LINE ( 'NONE', #10016, #13008 ) ;
#1823=CARTESIAN_POINT ( 'NONE',  ( 2.350558581813030123, 49.87752504164860312, 85.32593395802449265 ) ) ;
#1828=CARTESIAN_POINT ( 'NONE',  ( 0.5221537403065114047, 44.16218137147969713, 45.55433879953100273 ) ) ;
#1833=AXIS2_PLACEMENT_3D ( 'NONE', #12926, #16442, #9742 ) ;
#1853=CARTESIAN_POINT ( 'NONE',  ( -1.477846259693491149, 49.81903562097206617, 123.5543387995310098 ) ) ;
#1856=ORIENTED_EDGE ( 'NONE', *, *, #9229, .T. ) ;
#1859=FACE_OUTER_BOUND ( 'NONE', #20961, .T. ) ;
#1870=CARTESIAN_POINT ( 'NONE',  ( -1.306251101200015752, 49.87752504164858891, 85.32593395802449265 ) ) ;
#1895=PLANE ( 'NONE',  #19754 ) ;
#1903=FACE_OUTER_BOUND ( 'NONE', #5735, .T. ) ;
#1905=CARTESIAN_POINT ( 'NONE',  ( 28.52215374030649642, 44.16218137147969003, 87.85433879953103542 ) ) ;
#1912=FACE_OUTER_BOUND ( 'NONE', #18202, .T. ) ;
#1916=ORIENTED_EDGE ( 'NONE', *, *, #20288, .F. ) ;
#1928=DIRECTION ( 'NONE',  ( 1.779391786395883536E-16, 5.922860397471806844E-17, -1.000000000000000000 ) ) ;
#1932=EDGE_CURVE ( 'NONE', #667, #19622, #16292, .T. ) ;
#1935=LINE ( 'NONE', #6926, #20960 ) ;
#1951=ORIENTED_EDGE ( 'NONE', *, *, #10188, .T. ) ;
#1952=CARTESIAN_POINT ( 'NONE',  ( 1.855487073639847218, 49.49551470481303284, 77.82100546619766135 ) ) ;
#1955=DIRECTION ( 'NONE',  ( 0.000000000000000000, 1.000000000000000000, 0.000000000000000000 ) ) ;
#1959=CARTESIAN_POINT ( 'NONE',  ( 2.392664886727889240, 47.70104341108813628, 61.28382765310962554 ) ) ;
#1960=( BOUNDED_CURVE ( )  B_SPLINE_CURVE ( 3, ( #18246, #5048, #8468, #3568 ),
 .UNSPECIFIED., .F., .T. ) 
 B_SPLINE_CURVE_WITH_KNOTS ( ( 4, 4 ),
 ( 5.006904465492826972, 5.052225889838810602 ),
 .UNSPECIFIED. ) 
 CURVE ( )  GEOMETRIC_REPRESENTATION_ITEM ( )  RATIONAL_B_SPLINE_CURVE ( ( 1.000000000000000000, 0.9998288380325438540, 0.9998288380325438540, 1.000000000000000000 ) ) 
 REPRESENTATION_ITEM ( '' )  );
#1964=DIRECTION ( 'NONE',  ( 1.110223024625156540E-16, 1.000000000000000000, 5.922860397471808077E-17 ) ) ;
#1974=ORIENTED_EDGE ( 'NONE', *, *, #2689, .F. ) ;
#1975=DIRECTION ( 'NONE',  ( 2.043266227890062685E-16, 0.7071067811865451302, -0.7071067811865500152 ) ) ;
#1990=EDGE_CURVE ( 'NONE', #1268, #19018, #9262, .T. ) ;
#2009=DIRECTION ( 'NONE',  ( -3.211742425186504723E-16, 5.922860397471811774E-17, -1.000000000000000000 ) ) ;
#2023=DIRECTION ( 'NONE',  ( 2.043266227890062685E-16, 0.7071067811865451302, -0.7071067811865500152 ) ) ;
#2027=AXIS2_PLACEMENT_3D ( 'NONE', #12596, #18970, #11112 ) ;
#2032=VERTEX_POINT ( 'NONE', #20712 ) ;
#2053=ADVANCED_FACE ( 'NONE', ( #278 ), #9885, .F. ) ;
#2063=CARTESIAN_POINT ( 'NONE',  ( -1.306251101200014197, 49.87752504164859602, 53.32593395802448555 ) ) ;
#2096=DIRECTION ( 'NONE',  ( -2.267473790562806355E-16, 5.922860397471811774E-17, -1.000000000000000000 ) ) ;
#2114=LINE ( 'NONE', #3692, #2259 ) ;
#2123=CONICAL_SURFACE ( 'NONE', #6193, 4.000000000000003553, 0.7853981633974460586 ) ;
#2136=ORIENTED_EDGE ( 'NONE', *, *, #3471, .F. ) ;
#2137=ORIENTED_EDGE ( 'NONE', *, *, #15661, .T. ) ;
#2150=UNCERTAINTY_MEASURE_WITH_UNIT (LENGTH_MEASURE( 1.000000000000000082E-05 ), #2681, 'distance_accuracy_value', 'NONE');
#2160=CARTESIAN_POINT ( 'NONE',  ( -1.477846259693498254, 49.81903562097207327, 59.21119304902337888 ) ) ;
#2162=DIRECTION ( 'NONE',  ( -0.7071067811865535679, 1.203855704449247279E-16, -0.7071067811865414665 ) ) ;
#2165=CARTESIAN_POINT ( 'NONE',  ( 2.522153740306510628, 47.62628298661744708, 53.15433879953100416 ) ) ;
#2202=DIRECTION ( 'NONE',  ( -4.731737692062721725E-17, 0.7071067811865525687, 0.7071067811865425767 ) ) ;
#2207=ORIENTED_EDGE ( 'NONE', *, *, #15920, .T. ) ;
#2224=ORIENTED_EDGE ( 'NONE', *, *, #6602, .T. ) ;
#2232=DIRECTION ( 'NONE',  ( 1.000000000000000000, -1.110223024625156540E-16, 1.779391786395883043E-16 ) ) ;
#2234=CARTESIAN_POINT ( 'NONE',  ( -1.477846259693498920, 47.62628298661744708, 66.55433879953099563 ) ) ;
#2242=CARTESIAN_POINT ( 'NONE',  ( -1.477846259693502473, 47.62628298661744708, 74.55433879953100984 ) ) ;
#2252=LINE ( 'NONE', #19696, #1761 ) ;
#2259=VECTOR ( 'NONE', #20180, 1000.000000000000000 ) ;
#2262=DIRECTION ( 'NONE',  ( -1.000000000000000000, 0.000000000000000000, 0.000000000000000000 ) ) ;
#2263=DIRECTION ( 'NONE',  ( -1.779391786395883536E-16, -5.922860397471806844E-17, 1.000000000000000000 ) ) ;
#2267=DIRECTION ( 'NONE',  ( 1.779391786395883536E-16, 5.922860397471806844E-17, -1.000000000000000000 ) ) ;
#2268=CARTESIAN_POINT ( 'NONE',  ( 2.122153740306496505, 50.16218137147969713, 69.55433879953100984 ) ) ;
#2286=LINE ( 'NONE', #7389, #16302 ) ;
#2305=VERTEX_POINT ( 'NONE', #337 ) ;
#2312=CARTESIAN_POINT ( 'NONE',  ( 2.522153740306507075, 50.16218137147969713, 74.55433879953100984 ) ) ;
#2313=DIRECTION ( 'NONE',  ( 1.084202172485505420E-16, 1.000000000000000000, 0.000000000000000000 ) ) ;
#2314=CIRCLE ( 'NONE', #8775, 4.000000000000003553 ) ;
#2328=EDGE_CURVE ( 'NONE', #9181, #8749, #7593, .T. ) ;
#2334=CARTESIAN_POINT ( 'NONE',  ( 2.263811127080452845, 49.90383875825364157, 77.41268141275706682 ) ) ;
#2338=CARTESIAN_POINT ( 'NONE',  ( -1.477846259693499364, 47.62628298661744708, 69.15433879953098995 ) ) ;
#2366=DIRECTION ( 'NONE',  ( -9.598494438985367424E-18, 5.922860397471809309E-17, -1.000000000000000000 ) ) ;
#2367=CIRCLE ( 'NONE', #662, 3.999999999999996447 ) ;
#2376=DIRECTION ( 'NONE',  ( -1.110223024625156540E-16, -1.000000000000000000, -5.922860397471808077E-17 ) ) ;
#2407=PRODUCT_CONTEXT ( 'NONE', #11728, 'mechanical' ) ;
#2414=ORIENTED_EDGE ( 'NONE', *, *, #13793, .F. ) ;
#2435=CARTESIAN_POINT ( 'NONE',  ( 2.522153740306511516, 50.16218137147969713, 50.55433879953100273 ) ) ;
#2438=AXIS2_PLACEMENT_3D ( 'NONE', #6668, #19647, #16682 ) ;
#2444=ADVANCED_FACE ( 'NONE', ( #1416 ), #17690, .T. ) ;
#2446=DIRECTION ( 'NONE',  ( -4.731737692062685363E-17, 0.7071067811865536790, 0.7071067811865414665 ) ) ;
#2453=ORIENTED_EDGE ( 'NONE', *, *, #630, .F. ) ;
#2477=DIRECTION ( 'NONE',  ( 1.779391786395883536E-16, 5.922860397471805611E-17, -1.000000000000000000 ) ) ;
#2484=ADVANCED_FACE ( 'NONE', ( #20656 ), #14493, .T. ) ;
#2496=EDGE_CURVE ( 'NONE', #16100, #15360, #19007, .T. ) ;
#2519=EDGE_CURVE ( 'NONE', #11891, #7289, #17983, .T. ) ;
#2524=ORIENTED_EDGE ( 'NONE', *, *, #17073, .T. ) ;
#2529=ORIENTED_EDGE ( 'NONE', *, *, #16507, .F. ) ;
#2542=CARTESIAN_POINT ( 'NONE',  ( 1.215246153217547587, 50.28109722957945849, 83.67325465763077830 ) ) ;
#2579=CYLINDRICAL_SURFACE ( 'NONE', #18092, 6.000000000000001776 ) ;
#2620=EDGE_LOOP ( 'NONE', ( #20047, #13665, #8384, #10803, #9095, #3104, #13366, #8279, #8531, #17090, #3209, #16887, #13096, #6702, #13259, #9211, #3516, #10318, #9607, #15390, #89, #10911, #8733, #3179, #20477, #13924, #7805, #20552, #18372, #10236 ) ) ;
#2627=ORIENTED_EDGE ( 'NONE', *, *, #13685, .T. ) ;
#2636=ORIENTED_EDGE ( 'NONE', *, *, #12225, .T. ) ;
#2642=VECTOR ( 'NONE', #7234, 1000.000000000000000 ) ;
#2650=( BOUNDED_CURVE ( )  B_SPLINE_CURVE ( 3, ( #2334, #20298, #2653, #15427 ),
 .UNSPECIFIED., .F., .F. ) 
 B_SPLINE_CURVE_WITH_KNOTS ( ( 4, 4 ),
 ( 5.006904465492824308, 5.052225889838808826 ),
 .UNSPECIFIED. ) 
 CURVE ( )  GEOMETRIC_REPRESENTATION_ITEM ( )  RATIONAL_B_SPLINE_CURVE ( ( 1.000000000000000000, 0.9998288380325438540, 0.9998288380325438540, 1.000000000000000000 ) ) 
 REPRESENTATION_ITEM ( '' )  );
#2653=CARTESIAN_POINT ( 'NONE',  ( 2.436687528221640697, 49.84925249003585179, 77.23980501161587142 ) ) ;
#2666=CARTESIAN_POINT ( 'NONE',  ( 1.119863296874945791, 50.25084051303456789, 53.06567965797612629 ) ) ;
#2681=( LENGTH_UNIT ( ) NAMED_UNIT ( * ) SI_UNIT ( .MILLI., .METRE. ) );
#2689=EDGE_CURVE ( 'NONE', #4527, #20386, #7496, .T. ) ;
#2721=AXIS2_PLACEMENT_3D ( 'NONE', #16899, #2009, #19868 ) ;
#2727=VECTOR ( 'NONE', #6762, 1000.000000000000000 ) ;
#2729=ORIENTED_EDGE ( 'NONE', *, *, #11455, .T. ) ;
#2767=DIRECTION ( 'NONE',  ( -1.571217453038212812E-16, -0.7071067811865500152, -0.7071067811865451302 ) ) ;
#2772=CARTESIAN_POINT ( 'NONE',  ( -1.477846259693489372, 49.76218137147969856, 53.55433879953100273 ) ) ;
#2778=( BOUNDED_CURVE ( )  B_SPLINE_CURVE ( 3, ( #19908, #5332, #15034, #13436 ),
 .UNSPECIFIED., .F., .F. ) 
 B_SPLINE_CURVE_WITH_KNOTS ( ( 4, 4 ),
 ( 5.988669822071448046, 6.577700792287722642 ),
 .UNSPECIFIED. ) 
 CURVE ( )  GEOMETRIC_REPRESENTATION_ITEM ( )  RATIONAL_B_SPLINE_CURVE ( ( 1.000000000000000000, 0.9712952651971044071, 0.9712952651971044071, 1.000000000000000000 ) ) 
 REPRESENTATION_ITEM ( '' )  );
#2782=DIRECTION ( 'NONE',  ( 1.016439536705157818E-16, 1.000000000000000000, 0.000000000000000000 ) ) ;
#2788=AXIS2_PLACEMENT_3D ( 'NONE', #1345, #19415, #8041 ) ;
#2799=ORIENTED_EDGE ( 'NONE', *, *, #1657, .F. ) ;
#2802=CIRCLE ( 'NONE', #8578, 3.999999999999996447 ) ;
#2815=CARTESIAN_POINT ( 'NONE',  ( 2.522153740306506631, 47.62628298661744708, 74.55433879953100984 ) ) ;
#2822=VERTEX_POINT ( 'NONE', #10966 ) ;
#2831=ORIENTED_EDGE ( 'NONE', *, *, #1275, .T. ) ;
#2846=CARTESIAN_POINT ( 'NONE',  ( -1.077846259693492126, 50.16218137147969713, 53.55433879953100273 ) ) ;
#2848=CIRCLE ( 'NONE', #8629, 3.999999999999996447 ) ;
#2857=DIRECTION ( 'NONE',  ( -4.731737692062910312E-17, 0.7071067811865460184, 0.7071067811865490160 ) ) ;
#2867=ORIENTED_EDGE ( 'NONE', *, *, #17069, .F. ) ;
#2875=LINE ( 'NONE', #6160, #9956 ) ;
#2882=EDGE_CURVE ( 'NONE', #11984, #3927, #7966, .T. ) ;
#2887=DIRECTION ( 'NONE',  ( 1.000000000000000000, 0.000000000000000000, 0.000000000000000000 ) ) ;
#2888=ADVANCED_FACE ( 'NONE', ( #17750 ), #19331, .F. ) ;
#2898=VERTEX_POINT ( 'NONE', #6151 ) ;
#2899=( BOUNDED_CURVE ( )  B_SPLINE_CURVE ( 3, ( #4220, #7529, #8811, #13703 ),
 .UNSPECIFIED., .F., .F. ) 
 B_SPLINE_CURVE_WITH_KNOTS ( ( 4, 4 ),
 ( 2.801755744135676629, 3.481429563043917152 ),
 .UNSPECIFIED. ) 
 CURVE ( )  GEOMETRIC_REPRESENTATION_ITEM ( )  RATIONAL_B_SPLINE_CURVE ( ( 1.000000000000000000, 0.9618726943880426816, 0.9618726943880426816, 1.000000000000000000 ) ) 
 REPRESENTATION_ITEM ( '' )  );
#2905=CARTESIAN_POINT ( 'NONE',  ( -1.077846259693497677, 50.16218137147969713, 85.55433879953100984 ) ) ;
#2917=ORIENTED_EDGE ( 'NONE', *, *, #12729, .T. ) ;
#2929=ORIENTED_EDGE ( 'NONE', *, *, #17038, .F. ) ;
#2937=EDGE_LOOP ( 'NONE', ( #7779, #13147, #20779, #15730, #1589 ) ) ;
#2946=AXIS2_PLACEMENT_3D ( 'NONE', #8906, #807, #7293 ) ;
#2955=PLANE ( 'NONE',  #14249 ) ;
#2957=( GEOMETRIC_REPRESENTATION_CONTEXT ( 3 ) GLOBAL_UNCERTAINTY_ASSIGNED_CONTEXT ( ( #2150 ) ) GLOBAL_UNIT_ASSIGNED_CONTEXT ( ( #2681, #6381, #20852 ) ) REPRESENTATION_CONTEXT ( 'NONE', 'WORKASPACE' ) );
#2969=CARTESIAN_POINT ( 'NONE',  ( -1.077846259693496123, 49.76218137147969856, 77.55433879953099563 ) ) ;
#3014=ORIENTED_EDGE ( 'NONE', *, *, #11706, .T. ) ;
#3030=CARTESIAN_POINT ( 'NONE',  ( 0.5221537403065104055, 40.36218137147969998, 46.15433879953098284 ) ) ;
#3037=VECTOR ( 'NONE', #248, 1000.000000000000000 ) ;
#3045=CARTESIAN_POINT ( 'NONE',  ( -1.477846259693495146, 49.76218137147969856, 85.55433879953100984 ) ) ;
#3061=DIRECTION ( 'NONE',  ( 1.000000000000000000, 0.000000000000000000, 0.000000000000000000 ) ) ;
#3062=ADVANCED_FACE ( 'NONE', ( #13580 ), #5377, .T. ) ;
#3075=DIRECTION ( 'NONE',  ( -1.110223024625156540E-16, -1.000000000000000000, -5.922860397471808077E-17 ) ) ;
#3079=CARTESIAN_POINT ( 'NONE',  ( -1.477846259693491593, 47.62628298661744708, 53.15433879953100416 ) ) ;
#3089=ADVANCED_FACE ( 'NONE', ( #14975 ), #16471, .F. ) ;
#3103=DIRECTION ( 'NONE',  ( 1.779391786395883536E-16, 5.922860397471806844E-17, -1.000000000000000000 ) ) ;
#3104=ORIENTED_EDGE ( 'NONE', *, *, #9620, .F. ) ;
#3114=VECTOR ( 'NONE', #18035, 1000.000000000000000 ) ;
#3120=CARTESIAN_POINT ( 'NONE',  ( -1.219503646467433589, 49.90383875825363447, 77.41268141275706682 ) ) ;
#3123=ADVANCED_FACE ( 'NONE', ( #712 ), #7408, .F. ) ;
#3125=DIRECTION ( 'NONE',  ( -1.000000000000000000, 0.000000000000000000, 0.000000000000000000 ) ) ;
#3128=ADVANCED_FACE ( 'NONE', ( #10519 ), #5412, .T. ) ;
#3134=ORIENTED_EDGE ( 'NONE', *, *, #17130, .F. ) ;
#3137=DIRECTION ( 'NONE',  ( -0.7071067811865474617, 1.203855704449244074E-16, -0.7071067811865476838 ) ) ;
#3138=EDGE_CURVE ( 'NONE', #6753, #4999, #13695, .T. ) ;
#3153=CARTESIAN_POINT ( 'NONE',  ( 0.5221537403065118488, 48.16218137147969003, 45.55433879953100273 ) ) ;
#3158=VERTEX_POINT ( 'NONE', #9021 ) ;
#3179=ORIENTED_EDGE ( 'NONE', *, *, #9240, .F. ) ;
#3187=DIRECTION ( 'NONE',  ( 1.000000000000000000, -1.110223024625156417E-16, -1.111814006898795283E-16 ) ) ;
#3190=LINE ( 'NONE', #8294, #15904 ) ;
#3200=DIRECTION ( 'NONE',  ( -1.084202172485505420E-16, -1.000000000000000000, 0.000000000000000000 ) ) ;
#3205=CARTESIAN_POINT ( 'NONE',  ( 0.5221537403065117378, 47.36218137147970708, 45.55433879953100273 ) ) ;
#3209=ORIENTED_EDGE ( 'NONE', *, *, #14005, .F. ) ;
#3224=ORIENTED_EDGE ( 'NONE', *, *, #3889, .F. ) ;
#3234=EDGE_LOOP ( 'NONE', ( #806, #11118, #3898, #19176, #9040 ) ) ;
#3258=CARTESIAN_POINT ( 'NONE',  ( 29.77115333998618496, 40.36218137147969287, 87.85433879953102121 ) ) ;
#3272=FACE_OUTER_BOUND ( 'NONE', #10919, .T. ) ;
#3286=DIRECTION ( 'NONE',  ( -1.779391786395883536E-16, -5.922860397471806844E-17, 1.000000000000000000 ) ) ;
#3309=VECTOR ( 'NONE', #14694, 999.9999999999998863 ) ;
#3311=LINE ( 'NONE', #1411, #11368 ) ;
#3314=AXIS2_PLACEMENT_3D ( 'NONE', #18629, #15549, #12457 ) ;
#3319=ORIENTED_EDGE ( 'NONE', *, *, #1990, .T. ) ;
#3323=EDGE_LOOP ( 'NONE', ( #2799, #4202, #10900, #12902, #9815, #5671 ) ) ;
#3343=EDGE_CURVE ( 'NONE', #16809, #10923, #10218, .T. ) ;
#3350=FACE_OUTER_BOUND ( 'NONE', #17389, .T. ) ;
#3351=ORIENTED_EDGE ( 'NONE', *, *, #219, .F. ) ;
#3382=AXIS2_PLACEMENT_3D ( 'NONE', #11929, #10450, #3713 ) ;
#3387=PLANE ( 'NONE',  #9952 ) ;
#3405=CARTESIAN_POINT ( 'NONE',  ( 28.52215374030649642, 40.36218137147969287, 87.65433879953101837 ) ) ;
#3417=ORIENTED_EDGE ( 'NONE', *, *, #1042, .T. ) ;
#3421=CARTESIAN_POINT ( 'NONE',  ( 2.522153740306507075, 50.16218137147969713, 74.55433879953100984 ) ) ;
#3430=ORIENTED_EDGE ( 'NONE', *, *, #2519, .T. ) ;
#3434=CARTESIAN_POINT ( 'NONE',  ( 28.52215374030649642, 44.16218137147969003, 87.05433879953100984 ) ) ;
#3438=DIRECTION ( 'NONE',  ( -1.000000000000000000, 1.110223024625156540E-16, -1.779391786395883043E-16 ) ) ;
#3440=VERTEX_POINT ( 'NONE', #19925 ) ;
#3448=AXIS2_PLACEMENT_3D ( 'NONE', #1185, #10989, #4254 ) ;
#3471=EDGE_CURVE ( 'NONE', #15353, #16835, #19618, .T. ) ;
#3475=CARTESIAN_POINT ( 'NONE',  ( -1.077846259693481246, 47.82824192744437397, 69.55433879953100984 ) ) ;
#3495=CARTESIAN_POINT ( 'NONE',  ( -0.07555581626192713063, 50.25084051303456789, 61.06567965797611919 ) ) ;
#3510=CARTESIAN_POINT ( 'NONE',  ( 0.5221537403065112937, 44.16218137147969713, 46.35433879953098568 ) ) ;
#3514=EDGE_CURVE ( 'NONE', #10923, #6568, #18453, .T. ) ;
#3516=ORIENTED_EDGE ( 'NONE', *, *, #17661, .T. ) ;
#3521=ORIENTED_EDGE ( 'NONE', *, *, #17073, .F. ) ;
#3533=CARTESIAN_POINT ( 'NONE',  ( 1.365599874297942051, 40.36218137147969998, 46.22770477045764181 ) ) ;
#3535=CARTESIAN_POINT ( 'NONE',  ( -1.306251101200017084, 49.87752504164859602, 69.32593395802447844 ) ) ;
#3536=EDGE_CURVE ( 'NONE', #7189, #12515, #6452, .T. ) ;
#3545=ORIENTED_EDGE ( 'NONE', *, *, #11849, .T. ) ;
#3568=CARTESIAN_POINT ( 'NONE',  ( 2.522153740306510628, 49.81903562097208038, 53.15433879953100416 ) ) ;
#3592=LINE ( 'NONE', #14986, #5994 ) ;
#3604=CARTESIAN_POINT ( 'NONE',  ( 28.52215374030649642, 48.16218137147969003, 87.85433879953103542 ) ) ;
#3658=FACE_OUTER_BOUND ( 'NONE', #6026, .T. ) ;
#3670=CARTESIAN_POINT ( 'NONE',  ( 0.5221537403065008576, 44.16218137147969003, 105.5543387995310098 ) ) ;
#3677=ADVANCED_FACE ( 'NONE', ( #9724 ), #9516, .F. ) ;
#3679=DIRECTION ( 'NONE',  ( -0.7071067811865535679, 1.203855704449247279E-16, -0.7071067811865414665 ) ) ;
#3692=CARTESIAN_POINT ( 'NONE',  ( 1.855487073639850104, 49.49551470481303994, 61.82100546619766845 ) ) ;
#3695=CARTESIAN_POINT ( 'NONE',  ( 2.122153740306496505, 47.82824192744437397, 69.55433879953100984 ) ) ;
#3704=VERTEX_POINT ( 'NONE', #1629 ) ;
#3707=DIRECTION ( 'NONE',  ( 1.779391786395883536E-16, 5.922860397471806844E-17, -1.000000000000000000 ) ) ;
#3710=AXIS2_PLACEMENT_3D ( 'NONE', #17285, #13776, #10820 ) ;
#3713=DIRECTION ( 'NONE',  ( 0.000000000000000000, 1.000000000000000000, 0.000000000000000000 ) ) ;
#3731=LINE ( 'NONE', #864, #19741 ) ;
#3774=EDGE_CURVE ( 'NONE', #2822, #12006, #14697, .T. ) ;
#3784=LINE ( 'NONE', #12001, #14954 ) ;
#3785=CARTESIAN_POINT ( 'NONE',  ( 2.263811127080454622, 49.90383875825364157, 69.41268141275703840 ) ) ;
#3832=DIRECTION ( 'NONE',  ( -1.110223024625156540E-16, -1.000000000000000000, -5.922860397471808077E-17 ) ) ;
#3846=EDGE_LOOP ( 'NONE', ( #605, #9938, #3521, #6606 ) ) ;
#3864=ORIENTED_EDGE ( 'NONE', *, *, #15312, .T. ) ;
#3873=DIRECTION ( 'NONE',  ( -3.211742425186504723E-16, 5.922860397471811774E-17, -1.000000000000000000 ) ) ;
#3874=ORIENTED_EDGE ( 'NONE', *, *, #17712, .F. ) ;
#3889=EDGE_CURVE ( 'NONE', #7228, #11865, #9311, .T. ) ;
#3891=ORIENTED_EDGE ( 'NONE', *, *, #12338, .F. ) ;
#3898=ORIENTED_EDGE ( 'NONE', *, *, #7248, .F. ) ;
#3904=CARTESIAN_POINT ( 'NONE',  ( -1.477846259693484265, 49.81903562097206617, 123.5543387995310098 ) ) ;
#3927=VERTEX_POINT ( 'NONE', #18847 ) ;
#3943=DIRECTION ( 'NONE',  ( -1.779391786395883536E-16, -5.922860397471806844E-17, 1.000000000000000000 ) ) ;
#3952=CIRCLE ( 'NONE', #5295, 3.999999999999996447 ) ;
#3985=CARTESIAN_POINT ( 'NONE',  ( 2.522153740306509295, 49.81903562097208038, 61.15433879953099705 ) ) ;
#3993=CARTESIAN_POINT ( 'NONE',  ( 2.522153740306509739, 50.16218137147969713, 61.15433879953099705 ) ) ;
#3994=ORIENTED_EDGE ( 'NONE', *, *, #6614, .F. ) ;
#3999=DIRECTION ( 'NONE',  ( -1.000000000000000000, 1.110223024625156540E-16, 6.575695984913707633E-33 ) ) ;
#4002=ORIENTED_EDGE ( 'NONE', *, *, #17038, .T. ) ;
#4011=PLANE ( 'NONE',  #19781 ) ;
#4019=VECTOR ( 'NONE', #2376, 1000.000000000000000 ) ;
#4020=ORIENTED_EDGE ( 'NONE', *, *, #14005, .T. ) ;
#4022=CARTESIAN_POINT ( 'NONE',  ( 0.5221537403065078520, 50.16218137147969713, 69.15433879953098995 ) ) ;
#4042=CARTESIAN_POINT ( 'NONE',  ( -1.219503646467429814, 49.90383875825364157, 53.41268141275706682 ) ) ;
#4043=CARTESIAN_POINT ( 'NONE',  ( -1.219503646467433144, 49.90383875825363447, 85.41268141275706682 ) ) ;
#4055=CARTESIAN_POINT ( 'NONE',  ( -0.1709386726045610538, 50.28109722957944427, 59.67325465763076409 ) ) ;
#4069=VECTOR ( 'NONE', #4638, 1000.000000000000000 ) ;
#4082=( GEOMETRIC_REPRESENTATION_CONTEXT ( 3 ) GLOBAL_UNCERTAINTY_ASSIGNED_CONTEXT ( ( #4853 ) ) GLOBAL_UNIT_ASSIGNED_CONTEXT ( ( #4544, #14441, #20817 ) ) REPRESENTATION_CONTEXT ( 'NONE', 'WORKASPACE' ) );
#4085=CARTESIAN_POINT ( 'NONE',  ( 2.122153740306511605, 49.76218137147969856, 61.55433879953100273 ) ) ;
#4094=CARTESIAN_POINT ( 'NONE',  ( -1.477846259693502917, 47.62628298661744708, 77.15433879953100416 ) ) ;
#4103=ORIENTED_EDGE ( 'NONE', *, *, #16099, .T. ) ;
#4112=DIRECTION ( 'NONE',  ( -1.779391786395883536E-16, -5.922860397471806844E-17, 1.000000000000000000 ) ) ;
#4115=FACE_OUTER_BOUND ( 'NONE', #14509, .T. ) ;
#4124=VECTOR ( 'NONE', #15508, 999.9999999999998863 ) ;
#4128=( BOUNDED_CURVE ( )  B_SPLINE_CURVE ( 3, ( #7894, #14165, #17262, #4269 ),
 .UNSPECIFIED., .F., .F. ) 
 B_SPLINE_CURVE_WITH_KNOTS ( ( 4, 4 ),
 ( 4.188790204786388749, 4.300872134317200945 ),
 .UNSPECIFIED. ) 
 CURVE ( )  GEOMETRIC_REPRESENTATION_ITEM ( )  RATIONAL_B_SPLINE_CURVE ( ( 1.000000000000000000, 0.9989534107080366709, 0.9989534107080366709, 1.000000000000000000 ) ) 
 REPRESENTATION_ITEM ( '' )  );
#4135=LINE ( 'NONE', #9157, #13688 ) ;
#4140=EDGE_CURVE ( 'NONE', #13663, #18483, #14973, .T. ) ;
#4143=CARTESIAN_POINT ( 'NONE',  ( 2.522153740306506187, 49.81903562097208038, 77.15433879953100416 ) ) ;
#4170=CARTESIAN_POINT ( 'NONE',  ( -0.1709386726045608318, 50.28109722957944427, 75.67325465763074988 ) ) ;
#4189=VECTOR ( 'NONE', #10674, 1000.000000000000000 ) ;
#4195=CARTESIAN_POINT ( 'NONE',  ( 0.5221537403065364957, 44.16218137147969003, 123.5543387995310098 ) ) ;
#4198=EDGE_CURVE ( 'NONE', #19989, #618, #12966, .T. ) ;
#4199=ORIENTED_EDGE ( 'NONE', *, *, #4525, .F. ) ;
#4202=ORIENTED_EDGE ( 'NONE', *, *, #20540, .T. ) ;
#4204=CARTESIAN_POINT ( 'NONE',  ( 1.119863296874942460, 50.25084051303456789, 85.06567965797613340 ) ) ;
#4217=CARTESIAN_POINT ( 'NONE',  ( 0.5221537403065056315, 44.16218137147969713, 77.55433879953099563 ) ) ;
#4218=EDGE_LOOP ( 'NONE', ( #2917, #1856, #9625, #15410, #12660 ) ) ;
#4220=CARTESIAN_POINT ( 'NONE',  ( 2.522153740306492864, 49.81903562097208749, 51.21119304902340019 ) ) ;
#4222=CARTESIAN_POINT ( 'NONE',  ( -1.392380047608630544, 49.84925249003584469, 61.23980501161588563 ) ) ;
#4249=( BOUNDED_CURVE ( )  B_SPLINE_CURVE ( 3, ( #1699, #8178, #14665, #3079 ),
 .UNSPECIFIED., .F., .F. ) 
 B_SPLINE_CURVE_WITH_KNOTS ( ( 4, 4 ),
 ( 1.982313172862385731, 2.094395102393197483 ),
 .UNSPECIFIED. ) 
 CURVE ( )  GEOMETRIC_REPRESENTATION_ITEM ( )  RATIONAL_B_SPLINE_CURVE ( ( 1.000000000000000000, 0.9989534107080366709, 0.9989534107080366709, 1.000000000000000000 ) ) 
 REPRESENTATION_ITEM ( '' )  );
#4254=DIRECTION ( 'NONE',  ( 1.084202172485505420E-16, 1.000000000000000000, 0.000000000000000000 ) ) ;
#4255=ORIENTED_EDGE ( 'NONE', *, *, #5063, .T. ) ;
#4269=CARTESIAN_POINT ( 'NONE',  ( 2.122153740306507164, 47.82824192744436687, 85.55433879953100984 ) ) ;
#4273=DIRECTION ( 'NONE',  ( 1.110223024625156540E-16, 1.000000000000000000, 5.922860397471808077E-17 ) ) ;
#4308=DIRECTION ( 'NONE',  ( -1.779391786395883536E-16, -5.922860397471806844E-17, 1.000000000000000000 ) ) ;
#4327=EDGE_CURVE ( 'NONE', #5606, #10143, #6692, .T. ) ;
#4330=AXIS2_PLACEMENT_3D ( 'NONE', #5939, #3137, #17325 ) ;
#4334=LINE ( 'NONE', #12440, #1449 ) ;
#4347=CARTESIAN_POINT ( 'NONE',  ( 2.522153740306507519, 47.62628298661744708, 69.15433879953098995 ) ) ;
#4348=LINE ( 'NONE', #2772, #13039 ) ;
#4359=VERTEX_POINT ( 'NONE', #5199 ) ;
#4365=AXIS2_PLACEMENT_3D ( 'NONE', #3434, #8336, #14918 ) ;
#4398=ORIENTED_EDGE ( 'NONE', *, *, #5211, .F. ) ;
#4415=EDGE_LOOP ( 'NONE', ( #16356, #2524, #9337, #6805, #12005 ) ) ;
#4421=DIRECTION ( 'NONE',  ( 1.110223024625156540E-16, 1.000000000000000000, 5.922860397471808077E-17 ) ) ;
#4433=ORIENTED_EDGE ( 'NONE', *, *, #5438, .T. ) ;
#4435=DIRECTION ( 'NONE',  ( -1.571217453038212812E-16, -0.7071067811865500152, -0.7071067811865451302 ) ) ;
#4459=DIRECTION ( 'NONE',  ( -0.7071067811865474617, 1.203855704449244074E-16, -0.7071067811865476838 ) ) ;
#4493=DIRECTION ( 'NONE',  ( -1.084202172485505420E-16, -1.000000000000000000, 0.000000000000000000 ) ) ;
#4494=ORIENTED_EDGE ( 'NONE', *, *, #13092, .F. ) ;
#4506=ORIENTED_EDGE ( 'NONE', *, *, #1024, .T. ) ;
#4515=VECTOR ( 'NONE', #3832, 1000.000000000000000 ) ;
#4525=EDGE_CURVE ( 'NONE', #15383, #15567, #1349, .T. ) ;
#4527=VERTEX_POINT ( 'NONE', #14636 ) ;
#4544=( LENGTH_UNIT ( ) NAMED_UNIT ( * ) SI_UNIT ( .MILLI., .METRE. ) );
#4586=DIRECTION ( 'NONE',  ( 0.7071067811865539010, -3.662367542345418158E-17, -0.7071067811865411334 ) ) ;
#4609=LINE ( 'NONE', #20881, #10547 ) ;
#4623=EDGE_LOOP ( 'NONE', ( #7614, #19859, #10727, #6571 ) ) ;
#4629=EDGE_LOOP ( 'NONE', ( #5969, #10610, #14836, #9981, #17816, #14435 ) ) ;
#4638=DIRECTION ( 'NONE',  ( 1.000000000000000000, -1.110223024625156540E-16, 1.779391786395883043E-16 ) ) ;
#4646=CARTESIAN_POINT ( 'NONE',  ( 1.855487073639841000, 49.49551470481302573, 69.82100546619766135 ) ) ;
#4655=DIRECTION ( 'NONE',  ( -2.267473790562806355E-16, 5.922860397471811774E-17, -1.000000000000000000 ) ) ;
#4658=AXIS2_PLACEMENT_3D ( 'NONE', #18051, #8269, #8159 ) ;
#4660=CARTESIAN_POINT ( 'NONE',  ( 0.5221537403065118488, 48.16218137147969003, 45.55433879953100273 ) ) ;
#4671=CARTESIAN_POINT ( 'NONE',  ( 27.27315414062681853, 40.36218137147969287, 87.85433879953103542 ) ) ;
#4688=ORIENTED_EDGE ( 'NONE', *, *, #16483, .F. ) ;
#4690=AXIS2_PLACEMENT_3D ( 'NONE', #2905, #786, #13761 ) ;
#4696=ORIENTED_EDGE ( 'NONE', *, *, #5660, .F. ) ;
#4704=CARTESIAN_POINT ( 'NONE',  ( 2.522153740306495529, 49.81903562097208749, 83.21119304902340730 ) ) ;
#4708=CIRCLE ( 'NONE', #4365, 3.199999999999987743 ) ;
#4724=AXIS2_PLACEMENT_3D ( 'NONE', #8702, #10202, #8380 ) ;
#4730=ORIENTED_EDGE ( 'NONE', *, *, #1419, .F. ) ;
#4734=VECTOR ( 'NONE', #15789, 1000.000000000000000 ) ;
#4748=AXIS2_PLACEMENT_3D ( 'NONE', #17464, #10887, #2887 ) ;
#4763=DIRECTION ( 'NONE',  ( 1.084202172485505420E-16, 1.000000000000000000, 0.000000000000000000 ) ) ;
#4773=DIRECTION ( 'NONE',  ( -1.779391786395883783E-16, -5.922860397471806844E-17, 1.000000000000000000 ) ) ;
#4774=CARTESIAN_POINT ( 'NONE',  ( 0.5221537403065042993, 44.16218137147969713, 85.55433879953100984 ) ) ;
#4775=EDGE_CURVE ( 'NONE', #618, #3158, #7878, .T. ) ;
#4789=EDGE_CURVE ( 'NONE', #2032, #2305, #19381, .T. ) ;
#4799=DIRECTION ( 'NONE',  ( -1.000000000000000000, 1.110223024625156540E-16, -1.779391786395883043E-16 ) ) ;
#4801=( BOUNDED_CURVE ( )  B_SPLINE_CURVE ( 3, ( #3120, #9623, #1527, #8943 ),
 .UNSPECIFIED., .F., .F. ) 
 B_SPLINE_CURVE_WITH_KNOTS ( ( 4, 4 ),
 ( 5.988669822071447157, 6.577700792287721754 ),
 .UNSPECIFIED. ) 
 CURVE ( )  GEOMETRIC_REPRESENTATION_ITEM ( )  RATIONAL_B_SPLINE_CURVE ( ( 1.000000000000000000, 0.9712952651971044071, 0.9712952651971044071, 1.000000000000000000 ) ) 
 REPRESENTATION_ITEM ( '' )  );
#4804=PLANE ( 'NONE',  #6841 ) ;
#4806=ORIENTED_EDGE ( 'NONE', *, *, #16023, .T. ) ;
#4828=VERTEX_POINT ( 'NONE', #3604 ) ;
#4837=VERTEX_POINT ( 'NONE', #10334 ) ;
#4853=UNCERTAINTY_MEASURE_WITH_UNIT (LENGTH_MEASURE( 1.000000000000000082E-05 ), #4544, 'distance_accuracy_value', 'NONE');
#4857=AXIS2_PLACEMENT_3D ( 'NONE', #6529, #20983, #11346 ) ;
#4867=DIRECTION ( 'NONE',  ( -1.571217453038212812E-16, -0.7071067811865500152, -0.7071067811865451302 ) ) ;
#4892=CARTESIAN_POINT ( 'NONE',  ( 1.771153339986189845, 40.36218137147969998, 46.35433879953098568 ) ) ;
#4922=LINE ( 'NONE', #12815, #7252 ) ;
#4930=EDGE_CURVE ( 'NONE', #13218, #2822, #20914, .T. ) ;
#4941=CARTESIAN_POINT ( 'NONE',  ( 0.5221537403065081850, 50.16218137147969713, 67.55433879953099563 ) ) ;
#4987=CARTESIAN_POINT ( 'NONE',  ( 2.263811127080450625, 49.90383875825364157, 85.41268141275705261 ) ) ;
#4989=EDGE_LOOP ( 'NONE', ( #5014, #13382, #18582, #5579 ) ) ;
#4994=DIRECTION ( 'NONE',  ( -1.000000000000000000, 1.110223024625156294E-16, 2.267473790562806848E-16 ) ) ;
#4999=VERTEX_POINT ( 'NONE', #11272 ) ;
#5001=EDGE_CURVE ( 'NONE', #11406, #7289, #6454, .T. ) ;
#5004=DIRECTION ( 'NONE',  ( 1.084202172485505420E-16, 1.000000000000000000, 0.000000000000000000 ) ) ;
#5008=CARTESIAN_POINT ( 'NONE',  ( 2.522153740306509739, 50.16218137147969713, 61.15433879953099705 ) ) ;
#5009=ADVANCED_FACE ( 'NONE', ( #3272 ), #2955, .F. ) ;
#5014=ORIENTED_EDGE ( 'NONE', *, *, #3536, .F. ) ;
#5017=AXIS2_PLACEMENT_3D ( 'NONE', #9278, #5958, #20531 ) ;
#5021=ORIENTED_EDGE ( 'NONE', *, *, #6845, .F. ) ;
#5048=CARTESIAN_POINT ( 'NONE',  ( 2.350558581813038117, 49.87752504164859602, 53.32593395802448555 ) ) ;
#5053=DIRECTION ( 'NONE',  ( -2.267473790562806355E-16, 5.922860397471811774E-17, -1.000000000000000000 ) ) ;
#5060=EDGE_CURVE ( 'NONE', #14869, #13044, #2367, .T. ) ;
#5063=EDGE_CURVE ( 'NONE', #12696, #16856, #13486, .T. ) ;
#5068=VECTOR ( 'NONE', #11167, 999.9999999999998863 ) ;
#5075=ORIENTED_EDGE ( 'NONE', *, *, #8577, .T. ) ;
#5094=EDGE_CURVE ( 'NONE', #667, #17901, #20005, .T. ) ;
#5097=CARTESIAN_POINT ( 'NONE',  ( 2.522153740306511960, 47.62628298661745418, 45.55433879953100273 ) ) ;
#5116=DIRECTION ( 'NONE',  ( -0.5773502691896219563, 0.5773502691896226224, -0.5773502691896327255 ) ) ;
#5120=AXIS2_PLACEMENT_3D ( 'NONE', #14736, #6743, #1964 ) ;
#5123=CARTESIAN_POINT ( 'NONE',  ( -1.392380047608623883, 49.84925249003585179, 77.23980501161587142 ) ) ;
#5131=DIRECTION ( 'NONE',  ( -1.110223024625156540E-16, -1.000000000000000000, -5.922860397471808077E-17 ) ) ;
#5139=CARTESIAN_POINT ( 'NONE',  ( 2.522153740306506631, 49.16218137147969003, 74.55433879953100984 ) ) ;
#5150=ORIENTED_EDGE ( 'NONE', *, *, #11988, .F. ) ;
#5152=DIRECTION ( 'NONE',  ( 1.000000000000000000, -1.110223024625156540E-16, 1.779391786395883043E-16 ) ) ;
#5170=ORIENTED_EDGE ( 'NONE', *, *, #10100, .F. ) ;
#5181=ORIENTED_EDGE ( 'NONE', *, *, #18553, .T. ) ;
#5199=CARTESIAN_POINT ( 'NONE',  ( -1.219503646467433589, 49.90383875825363447, 77.41268141275706682 ) ) ;
#5203=ORIENTED_EDGE ( 'NONE', *, *, #10660, .F. ) ;
#5211=EDGE_CURVE ( 'NONE', #2305, #7517, #1695, .T. ) ;
#5272=ORIENTED_EDGE ( 'NONE', *, *, #3138, .F. ) ;
#5282=DIRECTION ( 'NONE',  ( -1.000000000000000000, 1.110223024625156540E-16, -1.779391786395883043E-16 ) ) ;
#5286=CARTESIAN_POINT ( 'NONE',  ( 2.522153740306507519, 47.62628298661744708, 69.15433879953098995 ) ) ;
#5292=CARTESIAN_POINT ( 'NONE',  ( 28.52215374030649642, 47.36218137147967155, 87.05433879953100984 ) ) ;
#5295=AXIS2_PLACEMENT_3D ( 'NONE', #17364, #17669, #7784 ) ;
#5321=EDGE_CURVE ( 'NONE', #16316, #14474, #11863, .T. ) ;
#5332=CARTESIAN_POINT ( 'NONE',  ( -0.07555581626192474365, 50.25084051303456079, 69.06567965797609077 ) ) ;
#5336=CARTESIAN_POINT ( 'NONE',  ( -1.477846259693498920, 49.81903562097206617, 75.21119304902337888 ) ) ;
#5337=AXIS2_PLACEMENT_3D ( 'NONE', #1905, #3286, #196 ) ;
#5338=ORIENTED_EDGE ( 'NONE', *, *, #15993, .T. ) ;
#5343=B_SPLINE_CURVE_WITH_KNOTS ( 'NONE', 3,
 ( #12304, #12088, #18786, #1011 ),
 .UNSPECIFIED., .F., .F.,
 ( 4, 4 ),
 ( 0.01428392225856168346, 0.01552286970674640783 ),
 .UNSPECIFIED. ) ;
#5349=CARTESIAN_POINT ( 'NONE',  ( -1.477846259693492925, 47.62628298661744708, 45.55433879953100273 ) ) ;
#5369=VECTOR ( 'NONE', #15364, 1000.000000000000000 ) ;
#5377=PLANE ( 'NONE',  #8486 ) ;
#5381=AXIS2_PLACEMENT_3D ( 'NONE', #18107, #1928, #8425 ) ;
#5384=DIRECTION ( 'NONE',  ( 1.110223024625156540E-16, 1.000000000000000000, 5.922860397471808077E-17 ) ) ;
#5397=CARTESIAN_POINT ( 'NONE',  ( 0.5221537403065105165, 44.16218137147969713, 50.55433879953100273 ) ) ;
#5409=CARTESIAN_POINT ( 'NONE',  ( -1.477846259693495146, 49.81903562097207327, 85.15433879953098995 ) ) ;
#5412=TOROIDAL_SURFACE ( 'NONE', #9198, 13.99999999999999645, 4.000000000000000000 ) ;
#5420=DIRECTION ( 'NONE',  ( -2.909222284125554245E-16, -0.7071067811865460184, 0.7071067811865490160 ) ) ;
#5432=ORIENTED_EDGE ( 'NONE', *, *, #10732, .F. ) ;
#5434=CARTESIAN_POINT ( 'NONE',  ( 2.392664886727894125, 47.70104341108812918, 77.28382765310962554 ) ) ;
#5435=EDGE_CURVE ( 'NONE', #14176, #16316, #20698, .T. ) ;
#5438=EDGE_CURVE ( 'NONE', #19018, #983, #2899, .T. ) ;
#5441=CARTESIAN_POINT ( 'NONE',  ( 2.522153740306493308, 49.81903562097208749, 59.21119304902340019 ) ) ;
#5451=CARTESIAN_POINT ( 'NONE',  ( 0.5221537403065064087, 48.16218137147969003, 66.55433879953099563 ) ) ;
#5491=ORIENTED_EDGE ( 'NONE', *, *, #11737, .T. ) ;
#5522=DIRECTION ( 'NONE',  ( -4.731737692062861008E-17, 0.7071067811865475727, 0.7071067811865475727 ) ) ;
#5525=AXIS2_PLACEMENT_3D ( 'NONE', #12495, #10918, #3125 ) ;
#5527=DIRECTION ( 'NONE',  ( 1.000000000000000000, 0.000000000000000000, 0.000000000000000000 ) ) ;
#5547=VERTEX_POINT ( 'NONE', #9028 ) ;
#5552=ORIENTED_EDGE ( 'NONE', *, *, #8407, .F. ) ;
#5579=ORIENTED_EDGE ( 'NONE', *, *, #12878, .T. ) ;
#5586=CARTESIAN_POINT ( 'NONE',  ( 2.436687528221645582, 49.84925249003584469, 61.23980501161587853 ) ) ;
#5593=FACE_OUTER_BOUND ( 'NONE', #17495, .T. ) ;
#5598=ORIENTED_EDGE ( 'NONE', *, *, #7248, .T. ) ;
#5606=VERTEX_POINT ( 'NONE', #17109 ) ;
#5620=( BOUNDED_CURVE ( )  B_SPLINE_CURVE ( 3, ( #19703, #5123, #7466, #13962 ),
 .UNSPECIFIED., .F., .F. ) 
 B_SPLINE_CURVE_WITH_KNOTS ( ( 4, 4 ),
 ( 1.230959417340772521, 1.276280841686757705 ),
 .UNSPECIFIED. ) 
 CURVE ( )  GEOMETRIC_REPRESENTATION_ITEM ( )  RATIONAL_B_SPLINE_CURVE ( ( 1.000000000000000000, 0.9998288380325438540, 0.9998288380325438540, 1.000000000000000000 ) ) 
 REPRESENTATION_ITEM ( '' )  );
#5636=CARTESIAN_POINT ( 'NONE',  ( 0.5221537403065077410, 44.16218137147969713, 66.55433879953099563 ) ) ;
#5660=EDGE_CURVE ( 'NONE', #18556, #20977, #20599, .T. ) ;
#5671=ORIENTED_EDGE ( 'NONE', *, *, #13786, .F. ) ;
#5695=EDGE_LOOP ( 'NONE', ( #14844, #11281, #1974, #5170, #17695 ) ) ;
#5706=LINE ( 'NONE', #9133, #14533 ) ;
#5735=EDGE_LOOP ( 'NONE', ( #2636, #17920, #14112, #20862, #12809 ) ) ;
#5736=PRODUCT_DEFINITION_CONTEXT ( 'detailed design', #5874, 'design' ) ;
#5739=EDGE_CURVE ( 'NONE', #8576, #8218, #6112, .T. ) ;
#5750=AXIS2_PLACEMENT_3D ( 'NONE', #8485, #390, #14971 ) ;
#5759=VERTEX_POINT ( 'NONE', #9870 ) ;
#5763=DIRECTION ( 'NONE',  ( -1.110223024625156540E-16, -1.000000000000000000, -5.922860397471808077E-17 ) ) ;
#5770=DIRECTION ( 'NONE',  ( -1.779391786395883536E-16, -5.922860397471806844E-17, 1.000000000000000000 ) ) ;
#5786=AXIS2_PLACEMENT_3D ( 'NONE', #14380, #12784, #19266 ) ;
#5793=ORIENTED_EDGE ( 'NONE', *, *, #14285, .F. ) ;
#5808=LINE ( 'NONE', #18896, #19778 ) ;
#5809=ORIENTED_EDGE ( 'NONE', *, *, #2882, .F. ) ;
#5813=EDGE_LOOP ( 'NONE', ( #17302, #15190, #8651, #2137, #11528 ) ) ;
#5821=ORIENTED_EDGE ( 'NONE', *, *, #8407, .T. ) ;
#5822=LINE ( 'NONE', #10641, #19626 ) ;
#5844=LINE ( 'NONE', #11278, #11292 ) ;
#5864=EDGE_CURVE ( 'NONE', #8749, #7909, #5343, .T. ) ;
#5874=APPLICATION_CONTEXT ( 'automotive_design' ) ;
#5886=AXIS2_PLACEMENT_3D ( 'NONE', #4217, #1353, #11149 ) ;
#5895=ORIENTED_EDGE ( 'NONE', *, *, #14085, .F. ) ;
#5899=DIRECTION ( 'NONE',  ( 4.142850521348543581E-16, -5.922860397471813007E-17, 1.000000000000000000 ) ) ;
#5939=CARTESIAN_POINT ( 'NONE',  ( 2.522153740306511072, 50.16218137147969713, 53.15433879953100416 ) ) ;
#5958=DIRECTION ( 'NONE',  ( 1.110223024625156540E-16, 1.000000000000000000, 5.922860397471808077E-17 ) ) ;
#5969=ORIENTED_EDGE ( 'NONE', *, *, #13793, .T. ) ;
#5970=PLANE ( 'NONE',  #14716 ) ;
#5980=VERTEX_POINT ( 'NONE', #17287 ) ;
#5994=VECTOR ( 'NONE', #10101, 1000.000000000000000 ) ;
#6010=COLOUR_RGB ( '', 0.31764706, 0.68627451, 0.89019608) ;
#6011=DIRECTION ( 'NONE',  ( -1.000000000000000000, 0.000000000000000000, 0.000000000000000000 ) ) ;
#6015=ORIENTED_EDGE ( 'NONE', *, *, #8319, .T. ) ;
#6026=EDGE_LOOP ( 'NONE', ( #2453, #344, #7866, #3430, #4806 ) ) ;
#6039=CARTESIAN_POINT ( 'NONE',  ( -1.477846259693499364, 49.81903562097207327, 83.21119304902337888 ) ) ;
#6053=FACE_OUTER_BOUND ( 'NONE', #4218, .T. ) ;
#6059=VECTOR ( 'NONE', #550, 1000.000000000000114 ) ;
#6069=CARTESIAN_POINT ( 'NONE',  ( 0.5221537403065064087, 48.16218137147969003, 85.55433879953100984 ) ) ;
#6102=ORIENTED_EDGE ( 'NONE', *, *, #8352, .F. ) ;
#6105=AXIS2_PLACEMENT_3D ( 'NONE', #19827, #16652, #256 ) ;
#6110=AXIS2_PLACEMENT_3D ( 'NONE', #15286, #7072, #7297 ) ;
#6112=CIRCLE ( 'NONE', #20370, 4.000000000000000000 ) ;
#6139=EDGE_CURVE ( 'NONE', #11984, #11711, #18016, .T. ) ;
#6148=CARTESIAN_POINT ( 'NONE',  ( -1.477846259693492037, 50.16218137147969713, 69.55433879953100984 ) ) ;
#6151=CARTESIAN_POINT ( 'NONE',  ( -1.477846259693491149, 47.62628298661744708, 50.55433879953100273 ) ) ;
#6152=CARTESIAN_POINT ( 'NONE',  ( -1.477846259693493813, 50.16218137147969713, 74.55433879953100984 ) ) ;
#6154=CIRCLE ( 'NONE', #18736, 3.999999999999996447 ) ;
#6160=CARTESIAN_POINT ( 'NONE',  ( -1.477846259693493813, 49.76218137147969856, 77.55433879953099563 ) ) ;
#6190=AXIS2_PLACEMENT_3D ( 'NONE', #9462, #14345, #10654 ) ;
#6192=DIRECTION ( 'NONE',  ( -1.110223024625156540E-16, -1.000000000000000000, -5.922860397471808077E-17 ) ) ;
#6193=AXIS2_PLACEMENT_3D ( 'NONE', #16844, #2263, #7146 ) ;
#6194=ORIENTED_EDGE ( 'NONE', *, *, #5660, .T. ) ;
#6213=ORIENTED_EDGE ( 'NONE', *, *, #2689, .T. ) ;
#6215=CARTESIAN_POINT ( 'NONE',  ( 2.122153740306507164, 47.82824192744436687, 85.55433879953100984 ) ) ;
#6224=ORIENTED_EDGE ( 'NONE', *, *, #12185, .T. ) ;
#6238=CIRCLE ( 'NONE', #20161, 4.000000000000003553 ) ;
#6239=VERTEX_POINT ( 'NONE', #5336 ) ;
#6249=DIRECTION ( 'NONE',  ( -1.779391786395883536E-16, -5.922860397471806844E-17, 1.000000000000000000 ) ) ;
#6253=DIRECTION ( 'NONE',  ( -1.110223024625156540E-16, -1.000000000000000000, -5.922860397471808077E-17 ) ) ;
#6283=CARTESIAN_POINT ( 'NONE',  ( -1.219503646467431590, 49.90383875825363447, 61.41268141275705972 ) ) ;
#6288=LINE ( 'NONE', #9818, #15088 ) ;
#6293=( BOUNDED_CURVE ( )  B_SPLINE_CURVE ( 3, ( #7541, #2542, #15946, #6039 ),
 .UNSPECIFIED., .F., .T. ) 
 B_SPLINE_CURVE_WITH_KNOTS ( ( 4, 4 ),
 ( 2.801755744135677961, 3.481429563043919373 ),
 .UNSPECIFIED. ) 
 CURVE ( )  GEOMETRIC_REPRESENTATION_ITEM ( )  RATIONAL_B_SPLINE_CURVE ( ( 1.000000000000000000, 0.9618726943880424596, 0.9618726943880424596, 1.000000000000000000 ) ) 
 REPRESENTATION_ITEM ( '' )  );
#6294=VERTEX_POINT ( 'NONE', #2165 ) ;
#6301=CARTESIAN_POINT ( 'NONE',  ( -1.477846259693506914, 47.62628298661743997, 85.15433879953098995 ) ) ;
#6314=DIRECTION ( 'NONE',  ( 1.110223024625156540E-16, 1.000000000000000000, 5.922860397471808077E-17 ) ) ;
#6340=DIRECTION ( 'NONE',  ( 1.000000000000000000, -1.110223024625156417E-16, -1.111814006898795283E-16 ) ) ;
#6345=EDGE_CURVE ( 'NONE', #3158, #20516, #4128, .T. ) ;
#6353=ADVANCED_FACE ( 'NONE', ( #14072 ), #9502, .F. ) ;
#6381=( NAMED_UNIT ( * ) PLANE_ANGLE_UNIT ( ) SI_UNIT ( $, .RADIAN. ) );
#6382=EDGE_CURVE ( 'NONE', #4837, #19613, #1404, .T. ) ;
#6384=VERTEX_POINT ( 'NONE', #6283 ) ;
#6408=ORIENTED_EDGE ( 'NONE', *, *, #1657, .T. ) ;
#6424=CIRCLE ( 'NONE', #3382, 4.000000000000003553 ) ;
#6452=CIRCLE ( 'NONE', #8840, 4.000000000000003553 ) ;
#6454=LINE ( 'NONE', #9359, #10878 ) ;
#6460=DIRECTION ( 'NONE',  ( 1.779391786395883536E-16, 5.922860397471805611E-17, -1.000000000000000000 ) ) ;
#6468=DIRECTION ( 'NONE',  ( 1.000000000000000000, -1.110223024625156417E-16, -1.111814006898795283E-16 ) ) ;
#6488=FACE_OUTER_BOUND ( 'NONE', #1435, .T. ) ;
#6499=CARTESIAN_POINT ( 'NONE',  ( -1.077846259693496123, 50.16218137147969713, 77.55433879953099563 ) ) ;
#6521=AXIS2_PLACEMENT_3D ( 'NONE', #5397, #11919, #13713 ) ;
#6525=CIRCLE ( 'NONE', #18424, 4.000000000000000000 ) ;
#6529=CARTESIAN_POINT ( 'NONE',  ( 28.52215374030649642, 44.16218137147969003, 105.5543387995310098 ) ) ;
#6534=DIRECTION ( 'NONE',  ( 1.084202172485505420E-16, 1.000000000000000000, 0.000000000000000000 ) ) ;
#6540=CARTESIAN_POINT ( 'NONE',  ( -1.477846259693495146, 49.81903562097207327, 85.15433879953098995 ) ) ;
#6545=ORIENTED_EDGE ( 'NONE', *, *, #16864, .F. ) ;
#6555=CARTESIAN_POINT ( 'NONE',  ( 0.5221537403065071858, 44.16218137147969713, 69.55433879953100984 ) ) ;
#6563=ORIENTED_EDGE ( 'NONE', *, *, #12873, .F. ) ;
#6568=VERTEX_POINT ( 'NONE', #4892 ) ;
#6571=ORIENTED_EDGE ( 'NONE', *, *, #6591, .T. ) ;
#6591=EDGE_CURVE ( 'NONE', #12515, #10923, #16567, .T. ) ;
#6596=EDGE_LOOP ( 'NONE', ( #10347, #5491, #5181, #17782, #6916, #10098, #15475, #12602, #19478, #4398, #10638, #13587, #6213, #5793, #3874, #14899, #9512, #20658, #2529, #17119, #19071, #8494, #19166, #6715, #18883, #14419, #659, #18939, #8255, #18210 ) ) ;
#6601=LINE ( 'NONE', #3421, #8645 ) ;
#6602=EDGE_CURVE ( 'NONE', #17901, #16856, #10130, .T. ) ;
#6606=ORIENTED_EDGE ( 'NONE', *, *, #11455, .F. ) ;
#6614=EDGE_CURVE ( 'NONE', #5547, #6239, #8953, .T. ) ;
#6626=EDGE_CURVE ( 'NONE', #2822, #3440, #15228, .T. ) ;
#6635=DIRECTION ( 'NONE',  ( -0.5773502691896252870, 0.5773502691896259531, -0.5773502691896259531 ) ) ;
#6668=CARTESIAN_POINT ( 'NONE',  ( 14.52215374030650175, 44.16218137147969003, 105.5543387995309956 ) ) ;
#6691=LINE ( 'NONE', #5097, #14655 ) ;
#6692=LINE ( 'NONE', #109, #12925 ) ;
#6702=ORIENTED_EDGE ( 'NONE', *, *, #8600, .F. ) ;
#6715=ORIENTED_EDGE ( 'NONE', *, *, #5321, .F. ) ;
#6733=CARTESIAN_POINT ( 'NONE',  ( 28.52215374030649642, 44.16218137147969003, 87.85433879953103542 ) ) ;
#6738=ADVANCED_FACE ( 'NONE', ( #20427 ), #15963, .F. ) ;
#6743=DIRECTION ( 'NONE',  ( -1.779391786395883536E-16, -5.922860397471805611E-17, 1.000000000000000000 ) ) ;
#6753=VERTEX_POINT ( 'NONE', #9477 ) ;
#6755=DIRECTION ( 'NONE',  ( -1.779391786395883536E-16, -5.922860397471806844E-17, 1.000000000000000000 ) ) ;
#6761=CARTESIAN_POINT ( 'NONE',  ( -1.077846259693481024, 49.76218137147968434, 69.55433879953100984 ) ) ;
#6762=DIRECTION ( 'NONE',  ( 1.110223024625156540E-16, 1.000000000000000000, 5.922860397471808077E-17 ) ) ;
#6789=LINE ( 'NONE', #98, #14187 ) ;
#6804=CARTESIAN_POINT ( 'NONE',  ( 27.67918635042538966, 40.36218137147969287, 87.72755528265716407 ) ) ;
#6805=ORIENTED_EDGE ( 'NONE', *, *, #17044, .T. ) ;
#6807=VECTOR ( 'NONE', #15929, 1000.000000000000000 ) ;
#6836=EDGE_LOOP ( 'NONE', ( #18727, #331, #5075, #12371, #16042 ) ) ;
#6841=AXIS2_PLACEMENT_3D ( 'NONE', #18007, #1744, #1630 ) ;
#6844=VECTOR ( 'NONE', #14352, 1000.000000000000000 ) ;
#6845=EDGE_CURVE ( 'NONE', #7909, #1280, #1282, .T. ) ;
#6862=( BOUNDED_CURVE ( )  B_SPLINE_CURVE ( 3, ( #16482, #3495, #13081, #18384 ),
 .UNSPECIFIED., .F., .F. ) 
 B_SPLINE_CURVE_WITH_KNOTS ( ( 4, 4 ),
 ( 5.988669822071448046, 6.577700792287722642 ),
 .UNSPECIFIED. ) 
 CURVE ( )  GEOMETRIC_REPRESENTATION_ITEM ( )  RATIONAL_B_SPLINE_CURVE ( ( 1.000000000000000000, 0.9712952651971044071, 0.9712952651971044071, 1.000000000000000000 ) ) 
 REPRESENTATION_ITEM ( '' )  );
#6873=ORIENTED_EDGE ( 'NONE', *, *, #13685, .F. ) ;
#6883=VERTEX_POINT ( 'NONE', #20929 ) ;
#6887=EDGE_CURVE ( 'NONE', #18875, #2898, #3190, .T. ) ;
#6888=AXIS2_PLACEMENT_3D ( 'NONE', #8546, #13532, #8434 ) ;
#6896=CARTESIAN_POINT ( 'NONE',  ( 0.5221537403065086291, 44.16218137147969713, 61.55433879953100273 ) ) ;
#6897=ADVANCED_FACE ( 'NONE', ( #14464 ), #16383, .T. ) ;
#6909=DIRECTION ( 'NONE',  ( 4.142850521348543581E-16, -5.922860397471813007E-17, 1.000000000000000000 ) ) ;
#6916=ORIENTED_EDGE ( 'NONE', *, *, #5739, .T. ) ;
#6926=CARTESIAN_POINT ( 'NONE',  ( -1.477846259693490261, 50.16218137147969713, 61.15433879953099705 ) ) ;
#6946=EDGE_CURVE ( 'NONE', #15405, #1280, #6789, .T. ) ;
#6965=CARTESIAN_POINT ( 'NONE',  ( 0.5221537403065117378, 47.36218137147970708, 45.55433879953100273 ) ) ;
#6980=FACE_OUTER_BOUND ( 'NONE', #12517, .T. ) ;
#6999=CARTESIAN_POINT ( 'NONE',  ( 1.215246153217546254, 50.28109722957945849, 67.67325465763076409 ) ) ;
#7010=DIRECTION ( 'NONE',  ( -9.598494438985368964E-18, 5.922860397471809309E-17, -1.000000000000000000 ) ) ;
#7015=VECTOR ( 'NONE', #8640, 1000.000000000000000 ) ;
#7024=ADVANCED_FACE ( 'NONE', ( #19401 ), #17811, .F. ) ;
#7072=DIRECTION ( 'NONE',  ( -9.598494438985368964E-18, 5.922860397471809309E-17, -1.000000000000000000 ) ) ;
#7074=EDGE_CURVE ( 'NONE', #15383, #19989, #1541, .T. ) ;
#7084=CARTESIAN_POINT ( 'NONE',  ( 2.522153740306510628, 49.81903562097208038, 53.15433879953100416 ) ) ;
#7094=CYLINDRICAL_SURFACE ( 'NONE', #2721, 6.000000000000001776 ) ;
#7097=AXIS2_PLACEMENT_3D ( 'NONE', #17273, #7904, #4799 ) ;
#7120=ORIENTED_EDGE ( 'NONE', *, *, #9272, .F. ) ;
#7121=DIRECTION ( 'NONE',  ( 1.110223024625156540E-16, 1.000000000000000000, 5.922860397471808077E-17 ) ) ;
#7125=AXIS2_PLACEMENT_3D ( 'NONE', #2435, #13710, #18182 ) ;
#7135=DIRECTION ( 'NONE',  ( -1.110223024625156540E-16, -1.000000000000000000, -5.922860397471808077E-17 ) ) ;
#7136=EDGE_LOOP ( 'NONE', ( #2207, #9929, #9442, #11011, #20480 ) ) ;
#7142=CARTESIAN_POINT ( 'NONE',  ( 29.77115333998617785, 40.36218137147969287, 105.5543387995310098 ) ) ;
#7146=DIRECTION ( 'NONE',  ( 0.000000000000000000, 1.000000000000000000, 0.000000000000000000 ) ) ;
#7152=CARTESIAN_POINT ( 'NONE',  ( 2.522153740306508407, 50.16218137147969713, 66.55433879953099563 ) ) ;
#7155=CARTESIAN_POINT ( 'NONE',  ( -1.219503646467429814, 49.90383875825364157, 53.41268141275706682 ) ) ;
#7173=ORIENTED_EDGE ( 'NONE', *, *, #11209, .T. ) ;
#7188=CARTESIAN_POINT ( 'NONE',  ( 0.5221537403065008576, 44.16218137147969003, 105.5543387995310098 ) ) ;
#7189=VERTEX_POINT ( 'NONE', #1052 ) ;
#7199=VERTEX_POINT ( 'NONE', #9035 ) ;
#7212=AXIS2_PLACEMENT_3D ( 'NONE', #16067, #3187, #20724 ) ;
#7228=VERTEX_POINT ( 'NONE', #16534 ) ;
#7229=ORIENTED_EDGE ( 'NONE', *, *, #12729, .F. ) ;
#7234=DIRECTION ( 'NONE',  ( -3.211742425186504723E-16, 5.922860397471811774E-17, -1.000000000000000000 ) ) ;
#7240=AXIS2_PLACEMENT_3D ( 'NONE', #18732, #10353, #18835 ) ;
#7248=EDGE_CURVE ( 'NONE', #20516, #15383, #349, .T. ) ;
#7250=VERTEX_POINT ( 'NONE', #13344 ) ;
#7252=VECTOR ( 'NONE', #14413, 1000.000000000000000 ) ;
#7289=VERTEX_POINT ( 'NONE', #5451 ) ;
#7293=DIRECTION ( 'NONE',  ( 1.000000000000000000, -1.110223024625156540E-16, 1.779391786395883043E-16 ) ) ;
#7297=DIRECTION ( 'NONE',  ( -1.000000000000000000, 0.000000000000000000, 0.000000000000000000 ) ) ;
#7329=CARTESIAN_POINT ( 'NONE',  ( 0.5221537403065050764, 50.16218137147969713, 85.15433879953098995 ) ) ;
#7357=CARTESIAN_POINT ( 'NONE',  ( -0.8111795930268322907, 49.49551470481303994, 61.82100546619766845 ) ) ;
#7362=CYLINDRICAL_SURFACE ( 'NONE', #17071, 3.999999999999996447 ) ;
#7366=LINE ( 'NONE', #17371, #4019 ) ;
#7389=CARTESIAN_POINT ( 'NONE',  ( 2.522153740306498193, 49.81903562097208038, 123.5543387995310098 ) ) ;
#7390=EDGE_CURVE ( 'NONE', #500, #11984, #18863, .T. ) ;
#7397=CARTESIAN_POINT ( 'NONE',  ( -1.219503646467433144, 49.90383875825363447, 85.41268141275706682 ) ) ;
#7399=SHAPE_DEFINITION_REPRESENTATION ( #18037, #209 ) ;
#7408=PLANE ( 'NONE',  #7461 ) ;
#7413=ORIENTED_EDGE ( 'NONE', *, *, #10710, .F. ) ;
#7414=DIRECTION ( 'NONE',  ( -1.110223024625156540E-16, -1.000000000000000000, -5.922860397471808077E-17 ) ) ;
#7447=DIRECTION ( 'NONE',  ( -1.779391786395883536E-16, -5.922860397471806844E-17, 1.000000000000000000 ) ) ;
#7457=VECTOR ( 'NONE', #6755, 1000.000000000000000 ) ;
#7461=AXIS2_PLACEMENT_3D ( 'NONE', #17303, #7520, #18688 ) ;
#7466=CARTESIAN_POINT ( 'NONE',  ( -1.306251101200015086, 49.87752504164859602, 77.32593395802449265 ) ) ;
#7472=CARTESIAN_POINT ( 'NONE',  ( 14.52215374030650175, 40.36218137147969287, 105.5543387995309956 ) ) ;
#7473=DIRECTION ( 'NONE',  ( -1.000000000000000000, 0.000000000000000000, 0.000000000000000000 ) ) ;
#7484=PLANE ( 'NONE',  #4690 ) ;
#7496=( BOUNDED_CURVE ( )  B_SPLINE_CURVE ( 3, ( #9264, #12344, #15847, #10546 ),
 .UNSPECIFIED., .F., .F. ) 
 B_SPLINE_CURVE_WITH_KNOTS ( ( 4, 4 ),
 ( 1.982313172862386397, 2.094395102393197927 ),
 .UNSPECIFIED. ) 
 CURVE ( )  GEOMETRIC_REPRESENTATION_ITEM ( )  RATIONAL_B_SPLINE_CURVE ( ( 1.000000000000000000, 0.9989534107080366709, 0.9989534107080366709, 1.000000000000000000 ) ) 
 REPRESENTATION_ITEM ( '' )  );
#7503=FACE_OUTER_BOUND ( 'NONE', #8539, .T. ) ;
#7507=VECTOR ( 'NONE', #17976, 1000.000000000000000 ) ;
#7508=ORIENTED_EDGE ( 'NONE', *, *, #1990, .F. ) ;
#7510=CARTESIAN_POINT ( 'NONE',  ( 2.263811127080453733, 49.90383875825364157, 61.41268141275705972 ) ) ;
#7513=CARTESIAN_POINT ( 'NONE',  ( -1.477846259693491149, 49.16218137147969003, 58.55433879953100984 ) ) ;
#7514=EDGE_CURVE ( 'NONE', #14664, #9181, #2314, .T. ) ;
#7517=VERTEX_POINT ( 'NONE', #12766 ) ;
#7520=DIRECTION ( 'NONE',  ( 0.7071067811865539010, -3.662367542345418158E-17, -0.7071067811865411334 ) ) ;
#7524=ORIENTED_EDGE ( 'NONE', *, *, #12338, .T. ) ;
#7529=CARTESIAN_POINT ( 'NONE',  ( 1.215246153217547365, 50.28109722957945138, 51.67325465763073566 ) ) ;
#7534=CARTESIAN_POINT ( 'NONE',  ( -1.477846259693498254, 49.81903562097207327, 59.21119304902337888 ) ) ;
#7538=ADVANCED_FACE ( 'NONE', ( #1277 ), #13194, .T. ) ;
#7541=CARTESIAN_POINT ( 'NONE',  ( 2.522153740306495529, 49.81903562097208749, 83.21119304902340730 ) ) ;
#7551=EDGE_CURVE ( 'NONE', #15360, #8218, #7769, .T. ) ;
#7558=VECTOR ( 'NONE', #3103, 1000.000000000000000 ) ;
#7571=CARTESIAN_POINT ( 'NONE',  ( 0.5221537403065114047, 44.16218137147969713, 45.55433879953100273 ) ) ;
#7587=CARTESIAN_POINT ( 'NONE',  ( 2.522153740306510183, 50.16218137147969713, 58.55433879953100984 ) ) ;
#7593=B_SPLINE_CURVE_WITH_KNOTS ( 'NONE', 3,
 ( #4671, #6804, #1505, #3405 ),
 .UNSPECIFIED., .F., .F.,
 ( 4, 4 ),
 ( 0.01304472255648652691, 0.01428392225856168346 ),
 .UNSPECIFIED. ) ;
#7614=ORIENTED_EDGE ( 'NONE', *, *, #3343, .F. ) ;
#7619=CIRCLE ( 'NONE', #130, 3.999999999999996447 ) ;
#7626=ORIENTED_EDGE ( 'NONE', *, *, #12708, .T. ) ;
#7631=ORIENTED_EDGE ( 'NONE', *, *, #21034, .F. ) ;
#7632=ORIENTED_EDGE ( 'NONE', *, *, #10439, .T. ) ;
#7714=EDGE_LOOP ( 'NONE', ( #6545, #2224, #14240, #696, #13479 ) ) ;
#7758=EDGE_LOOP ( 'NONE', ( #14190, #8199, #15402, #18015, #5203 ) ) ;
#7769=LINE ( 'NONE', #4660, #13518 ) ;
#7779=ORIENTED_EDGE ( 'NONE', *, *, #4930, .T. ) ;
#7784=DIRECTION ( 'NONE',  ( -1.084202172485505420E-16, -1.000000000000000000, 0.000000000000000000 ) ) ;
#7795=AXIS2_PLACEMENT_3D ( 'NONE', #12853, #1584, #11275 ) ;
#7805=ORIENTED_EDGE ( 'NONE', *, *, #7551, .T. ) ;
#7864=CARTESIAN_POINT ( 'NONE',  ( -0.7268458593731681461, 40.36218137147969998, 45.55433879953100273 ) ) ;
#7866=ORIENTED_EDGE ( 'NONE', *, *, #10660, .T. ) ;
#7878=LINE ( 'NONE', #11399, #7507 ) ;
#7894=CARTESIAN_POINT ( 'NONE',  ( 2.522153740306504854, 47.62628298661744708, 85.15433879953098995 ) ) ;
#7904=DIRECTION ( 'NONE',  ( -4.731737692062861008E-17, 0.7071067811865475727, 0.7071067811865475727 ) ) ;
#7909=VERTEX_POINT ( 'NONE', #3258 ) ;
#7920=ADVANCED_FACE ( 'NONE', ( #17934 ), #8364, .T. ) ;
#7927=EDGE_CURVE ( 'NONE', #15976, #15529, #1960, .T. ) ;
#7929=CYLINDRICAL_SURFACE ( 'NONE', #1698, 6.000000000000001776 ) ;
#7942=ORIENTED_EDGE ( 'NONE', *, *, #10188, .F. ) ;
#7950=DIRECTION ( 'NONE',  ( -1.110223024625156540E-16, -1.000000000000000000, -5.922860397471808077E-17 ) ) ;
#7954=CARTESIAN_POINT ( 'NONE',  ( 2.263811127080452845, 49.90383875825364157, 77.41268141275706682 ) ) ;
#7966=LINE ( 'NONE', #4646, #5068 ) ;
#7975=PLANE ( 'NONE',  #7212 ) ;
#7981=DIRECTION ( 'NONE',  ( -1.110223024625156540E-16, -1.000000000000000000, -5.922860397471808077E-17 ) ) ;
#8000=VERTEX_POINT ( 'NONE', #16243 ) ;
#8015=CARTESIAN_POINT ( 'NONE',  ( -1.214884381343054542, 47.76843358786783256, 85.41730067788145675 ) ) ;
#8041=DIRECTION ( 'NONE',  ( 1.000000000000000000, -1.110223024625156540E-16, 1.779391786395883043E-16 ) ) ;
#8075=DIRECTION ( 'NONE',  ( -1.000000000000000000, 0.000000000000000000, 0.000000000000000000 ) ) ;
#8110=ORIENTED_EDGE ( 'NONE', *, *, #4789, .T. ) ;
#8159=DIRECTION ( 'NONE',  ( -1.002887009549092588E-15, -1.000000000000000000, 0.000000000000000000 ) ) ;
#8175=AXIS2_PLACEMENT_3D ( 'NONE', #10982, #18625, #10772 ) ;
#8178=CARTESIAN_POINT ( 'NONE',  ( -1.214884381343048991, 47.76843358786783256, 53.41730067788145675 ) ) ;
#8194=PRODUCT_DEFINITION ( 'UNKNOWN', '', #8875, #5736 ) ;
#8199=ORIENTED_EDGE ( 'NONE', *, *, #18817, .T. ) ;
#8210=DIRECTION ( 'NONE',  ( 1.000000000000000000, 0.000000000000000000, 0.000000000000000000 ) ) ;
#8214=DIRECTION ( 'NONE',  ( -1.779391786395883536E-16, -5.922860397471806844E-17, 1.000000000000000000 ) ) ;
#8218=VERTEX_POINT ( 'NONE', #13228 ) ;
#8219=VECTOR ( 'NONE', #6253, 1000.000000000000000 ) ;
#8240=( BOUNDED_CURVE ( )  B_SPLINE_CURVE ( 3, ( #7397, #15395, #4204, #10509 ),
 .UNSPECIFIED., .F., .T. ) 
 B_SPLINE_CURVE_WITH_KNOTS ( ( 4, 4 ),
 ( 5.988669822071447157, 6.577700792287720866 ),
 .UNSPECIFIED. ) 
 CURVE ( )  GEOMETRIC_REPRESENTATION_ITEM ( )  RATIONAL_B_SPLINE_CURVE ( ( 1.000000000000000000, 0.9712952651971045182, 0.9712952651971045182, 1.000000000000000000 ) ) 
 REPRESENTATION_ITEM ( '' )  );
#8244=FACE_OUTER_BOUND ( 'NONE', #11900, .T. ) ;
#8255=ORIENTED_EDGE ( 'NONE', *, *, #11209, .F. ) ;
#8269=DIRECTION ( 'NONE',  ( -1.779391786395883783E-16, -5.922860397471806844E-17, 1.000000000000000000 ) ) ;
#8276=DIRECTION ( 'NONE',  ( -1.084202172485505420E-16, -1.000000000000000000, 0.000000000000000000 ) ) ;
#8279=ORIENTED_EDGE ( 'NONE', *, *, #17044, .F. ) ;
#8285=AXIS2_PLACEMENT_3D ( 'NONE', #9539, #9427, #6011 ) ;
#8294=CARTESIAN_POINT ( 'NONE',  ( -1.477846259693489372, 50.16218137147969713, 50.55433879953100273 ) ) ;
#8313=DIRECTION ( 'NONE',  ( -2.267473790562806848E-16, 5.922860397471811774E-17, -1.000000000000000000 ) ) ;
#8316=VERTEX_POINT ( 'NONE', #451 ) ;
#8319=EDGE_CURVE ( 'NONE', #8473, #6384, #16840, .T. ) ;
#8324=EDGE_CURVE ( 'NONE', #140, #19954, #13641, .T. ) ;
#8332=EDGE_LOOP ( 'NONE', ( #1524, #15135, #13442, #4020, #1668 ) ) ;
#8336=DIRECTION ( 'NONE',  ( -4.142850521348543581E-16, 5.922860397471813007E-17, -1.000000000000000000 ) ) ;
#8337=DIRECTION ( 'NONE',  ( -3.211742425186504723E-16, 5.922860397471811774E-17, -1.000000000000000000 ) ) ;
#8350=LINE ( 'NONE', #5139, #3037 ) ;
#8352=EDGE_CURVE ( 'NONE', #12006, #3927, #2778, .T. ) ;
#8364=PLANE ( 'NONE',  #17603 ) ;
#8380=DIRECTION ( 'NONE',  ( -1.110223024625156540E-16, -1.000000000000000000, -5.922860397471808077E-17 ) ) ;
#8384=ORIENTED_EDGE ( 'NONE', *, *, #16723, .F. ) ;
#8387=ORIENTED_EDGE ( 'NONE', *, *, #17707, .T. ) ;
#8388=FACE_OUTER_BOUND ( 'NONE', #15026, .T. ) ;
#8401=VECTOR ( 'NONE', #7981, 1000.000000000000000 ) ;
#8407=EDGE_CURVE ( 'NONE', #18186, #7909, #15247, .T. ) ;
#8425=DIRECTION ( 'NONE',  ( -1.084202172485505420E-16, -1.000000000000000000, 0.000000000000000000 ) ) ;
#8430=ORIENTED_EDGE ( 'NONE', *, *, #18862, .T. ) ;
#8433=ORIENTED_EDGE ( 'NONE', *, *, #8577, .F. ) ;
#8434=DIRECTION ( 'NONE',  ( -1.084202172485505420E-16, -1.000000000000000000, 0.000000000000000000 ) ) ;
#8438=CARTESIAN_POINT ( 'NONE',  ( -1.077846259693493680, 47.82824192744436687, 61.55433879953100273 ) ) ;
#8466=DIRECTION ( 'NONE',  ( 1.110223024625156540E-16, 1.000000000000000000, 5.922860397471808077E-17 ) ) ;
#8468=CARTESIAN_POINT ( 'NONE',  ( 2.436687528221644250, 49.84925249003584469, 53.23980501161587853 ) ) ;
#8473=VERTEX_POINT ( 'NONE', #1397 ) ;
#8485=CARTESIAN_POINT ( 'NONE',  ( 0.5221537403065114047, 44.16218137147969713, 45.55433879953100273 ) ) ;
#8486=AXIS2_PLACEMENT_3D ( 'NONE', #13280, #18373, #11788 ) ;
#8488=EDGE_LOOP ( 'NONE', ( #18672, #4494, #5150, #11992 ) ) ;
#8491=CARTESIAN_POINT ( 'NONE',  ( 2.522153740306498193, 49.81903562097208038, 123.5543387995310098 ) ) ;
#8494=ORIENTED_EDGE ( 'NONE', *, *, #20934, .F. ) ;
#8517=DIRECTION ( 'NONE',  ( -4.731737692062791983E-17, 0.7071067811865500152, 0.7071067811865451302 ) ) ;
#8520=CARTESIAN_POINT ( 'NONE',  ( 2.522153740306509295, 49.81903562097208038, 61.15433879953099705 ) ) ;
#8531=ORIENTED_EDGE ( 'NONE', *, *, #19087, .F. ) ;
#8539=EDGE_LOOP ( 'NONE', ( #4255, #16282, #12265, #11819, #20336, #11243, #19500, #5552, #632, #1565 ) ) ;
#8546=CARTESIAN_POINT ( 'NONE',  ( 0.5221537403065071858, 44.16218137147969713, 69.55433879953100984 ) ) ;
#8551=ORIENTED_EDGE ( 'NONE', *, *, #18068, .F. ) ;
#8553=ORIENTED_EDGE ( 'NONE', *, *, #19759, .F. ) ;
#8567=PLANE ( 'NONE',  #5120 ) ;
#8576=VERTEX_POINT ( 'NONE', #881 ) ;
#8577=EDGE_CURVE ( 'NONE', #1268, #15169, #7366, .T. ) ;
#8578=AXIS2_PLACEMENT_3D ( 'NONE', #16363, #9775, #8276 ) ;
#8588=CARTESIAN_POINT ( 'NONE',  ( 2.263811127080453733, 49.90383875825364157, 61.41268141275705972 ) ) ;
#8600=EDGE_CURVE ( 'NONE', #19441, #11891, #10484, .T. ) ;
#8616=CARTESIAN_POINT ( 'NONE',  ( 2.392664886727887463, 47.70104341108812918, 69.28382765310961133 ) ) ;
#8623=LINE ( 'NONE', #18605, #16726 ) ;
#8627=( BOUNDED_CURVE ( )  B_SPLINE_CURVE ( 3, ( #8588, #13370, #5586, #3985 ),
 .UNSPECIFIED., .F., .F. ) 
 B_SPLINE_CURVE_WITH_KNOTS ( ( 4, 4 ),
 ( 5.006904465492826084, 5.052225889838810602 ),
 .UNSPECIFIED. ) 
 CURVE ( )  GEOMETRIC_REPRESENTATION_ITEM ( )  RATIONAL_B_SPLINE_CURVE ( ( 1.000000000000000000, 0.9998288380325438540, 0.9998288380325438540, 1.000000000000000000 ) ) 
 REPRESENTATION_ITEM ( '' )  );
#8629=AXIS2_PLACEMENT_3D ( 'NONE', #9590, #9379, #12671 ) ;
#8640=DIRECTION ( 'NONE',  ( -1.779391786395883536E-16, -5.922860397471806844E-17, 1.000000000000000000 ) ) ;
#8645=VECTOR ( 'NONE', #14387, 1000.000000000000000 ) ;
#8651=ORIENTED_EDGE ( 'NONE', *, *, #16909, .T. ) ;
#8656=ORIENTED_EDGE ( 'NONE', *, *, #12708, .F. ) ;
#8697=ORIENTED_EDGE ( 'NONE', *, *, #17069, .T. ) ;
#8702=CARTESIAN_POINT ( 'NONE',  ( 2.522153740306506631, 50.16218137147969713, 77.15433879953100416 ) ) ;
#8721=ORIENTED_EDGE ( 'NONE', *, *, #9073, .T. ) ;
#8733=ORIENTED_EDGE ( 'NONE', *, *, #4789, .F. ) ;
#8749=VERTEX_POINT ( 'NONE', #12484 ) ;
#8752=AXIS2_PLACEMENT_3D ( 'NONE', #1378, #12553, #17232 ) ;
#8762=CARTESIAN_POINT ( 'NONE',  ( -1.477846259693489817, 49.16218137147969003, 50.55433879953100273 ) ) ;
#8775=AXIS2_PLACEMENT_3D ( 'NONE', #10461, #16926, #9589 ) ;
#8798=ORIENTED_EDGE ( 'NONE', *, *, #6845, .T. ) ;
#8811=CARTESIAN_POINT ( 'NONE',  ( -0.1709386726045580007, 50.28109722957945138, 51.67325465763072856 ) ) ;
#8835=ADVANCED_FACE ( 'NONE', ( #17480 ), #7484, .F. ) ;
#8840=AXIS2_PLACEMENT_3D ( 'NONE', #18660, #5899, #10810 ) ;
#8845=LINE ( 'NONE', #12357, #4515 ) ;
#8858=DIRECTION ( 'NONE',  ( 1.000000000000000000, -1.110223024625156540E-16, 1.779391786395883043E-16 ) ) ;
#8864=CARTESIAN_POINT ( 'NONE',  ( 2.259191861956070024, 47.76843358786783966, 77.41730067788147096 ) ) ;
#8867=EDGE_LOOP ( 'NONE', ( #10147, #6408 ) ) ;
#8875=PRODUCT_DEFINITION_FORMATION_WITH_SPECIFIED_SOURCE ( 'ANY', '', #10609, .NOT_KNOWN. ) ;
#8906=CARTESIAN_POINT ( 'NONE',  ( 0.5221537403065109606, 50.16218137147969713, 51.55433879953100273 ) ) ;
#8938=PLANE ( 'NONE',  #13690 ) ;
#8943=CARTESIAN_POINT ( 'NONE',  ( 2.263811127080452845, 49.90383875825364157, 77.41268141275706682 ) ) ;
#8953=LINE ( 'NONE', #15337, #2642 ) ;
#8982=CARTESIAN_POINT ( 'NONE',  ( 2.522153740306511960, 47.62628298661745418, 45.55433879953100273 ) ) ;
#9003=DIRECTION ( 'NONE',  ( -1.571217453038212812E-16, -0.7071067811865500152, -0.7071067811865451302 ) ) ;
#9004=EDGE_CURVE ( 'NONE', #20977, #6883, #11860, .T. ) ;
#9021=CARTESIAN_POINT ( 'NONE',  ( 2.522153740306504854, 47.62628298661744708, 85.15433879953098995 ) ) ;
#9026=ORIENTED_EDGE ( 'NONE', *, *, #8319, .F. ) ;
#9028=CARTESIAN_POINT ( 'NONE',  ( -1.477846259693493813, 49.81903562097207327, 77.15433879953100416 ) ) ;
#9035=CARTESIAN_POINT ( 'NONE',  ( 0.5221537403065064087, 48.16218137147969003, 69.55433879953100984 ) ) ;
#9040=ORIENTED_EDGE ( 'NONE', *, *, #4775, .F. ) ;
#9055=CARTESIAN_POINT ( 'NONE',  ( 2.263811127080455954, 49.90383875825364157, 53.41268141275705972 ) ) ;
#9058=FACE_OUTER_BOUND ( 'NONE', #4623, .T. ) ;
#9062=CARTESIAN_POINT ( 'NONE',  ( -1.477846259693496922, 49.81903562097207327, 51.21119304902337888 ) ) ;
#9064=ADVANCED_FACE ( 'NONE', ( #754 ), #20636, .T. ) ;
#9073=EDGE_CURVE ( 'NONE', #13698, #15976, #17441, .T. ) ;
#9075=VECTOR ( 'NONE', #14924, 1000.000000000000000 ) ;
#9079=FACE_OUTER_BOUND ( 'NONE', #3234, .T. ) ;
#9081=ORIENTED_EDGE ( 'NONE', *, *, #14019, .T. ) ;
#9095=ORIENTED_EDGE ( 'NONE', *, *, #18588, .T. ) ;
#9102=ORIENTED_EDGE ( 'NONE', *, *, #19345, .F. ) ;
#9103=VECTOR ( 'NONE', #10354, 1000.000000000000000 ) ;
#9107=ORIENTED_EDGE ( 'NONE', *, *, #6887, .T. ) ;
#9118=ADVANCED_FACE ( 'NONE', ( #8388 ), #14870, .F. ) ;
#9126=CARTESIAN_POINT ( 'NONE',  ( 2.522153740306505298, 50.16218137147969713, 83.55433879953099563 ) ) ;
#9133=CARTESIAN_POINT ( 'NONE',  ( 2.522153740306498193, 49.81903562097208038, 123.5543387995310098 ) ) ;
#9144=CARTESIAN_POINT ( 'NONE',  ( 2.522153740306507963, 50.16218137147969713, 69.15433879953098995 ) ) ;
#9146=LINE ( 'NONE', #9259, #19109 ) ;
#9157=CARTESIAN_POINT ( 'NONE',  ( -0.8111795930268366206, 49.49551470481303284, 85.82100546619767556 ) ) ;
#9181=VERTEX_POINT ( 'NONE', #10211 ) ;
#9188=FILL_AREA_STYLE_COLOUR ( '', #6010 ) ;
#9192=ADVANCED_FACE ( 'NONE', ( #6980 ), #13702, .F. ) ;
#9198=AXIS2_PLACEMENT_3D ( 'NONE', #20492, #12105, #3999 ) ;
#9204=ORIENTED_EDGE ( 'NONE', *, *, #14549, .T. ) ;
#9209=VECTOR ( 'NONE', #13515, 1000.000000000000000 ) ;
#9211=ORIENTED_EDGE ( 'NONE', *, *, #20151, .F. ) ;
#9218=ORIENTED_EDGE ( 'NONE', *, *, #6946, .T. ) ;
#9229=EDGE_CURVE ( 'NONE', #15854, #618, #5706, .T. ) ;
#9237=ORIENTED_EDGE ( 'NONE', *, *, #14809, .F. ) ;
#9238=VECTOR ( 'NONE', #843, 1000.000000000000000 ) ;
#9240=EDGE_CURVE ( 'NONE', #3158, #2032, #5822, .T. ) ;
#9243=DIRECTION ( 'NONE',  ( 1.779391786395883536E-16, 5.922860397471806844E-17, -1.000000000000000000 ) ) ;
#9249=CARTESIAN_POINT ( 'NONE',  ( 2.522153740306494196, 49.81903562097208749, 67.21119304902339309 ) ) ;
#9259=CARTESIAN_POINT ( 'NONE',  ( 2.522153740306511072, 50.16218137147969713, 53.15433879953100416 ) ) ;
#9262=LINE ( 'NONE', #10965, #11194 ) ;
#9264=CARTESIAN_POINT ( 'NONE',  ( -1.077846259693496345, 47.82824192744436687, 77.55433879953099563 ) ) ;
#9272=EDGE_CURVE ( 'NONE', #3440, #9317, #15833, .T. ) ;
#9275=CARTESIAN_POINT ( 'NONE',  ( 28.52215374030650352, 44.16218137147969003, 105.5543387995309956 ) ) ;
#9278=CARTESIAN_POINT ( 'NONE',  ( 14.52215374030650175, 44.16218137147969003, 105.5543387995309956 ) ) ;
#9279=ADVANCED_FACE ( 'NONE', ( #10745 ), #17207, .F. ) ;
#9283=AXIS2_PLACEMENT_3D ( 'NONE', #4195, #3873, #11871 ) ;
#9311=( BOUNDED_CURVE ( )  B_SPLINE_CURVE ( 3, ( #20214, #5434, #8864, #10785 ),
 .UNSPECIFIED., .F., .F. ) 
 B_SPLINE_CURVE_WITH_KNOTS ( ( 4, 4 ),
 ( 4.188790204786388749, 4.300872134317199169 ),
 .UNSPECIFIED. ) 
 CURVE ( )  GEOMETRIC_REPRESENTATION_ITEM ( )  RATIONAL_B_SPLINE_CURVE ( ( 1.000000000000000000, 0.9989534107080366709, 0.9989534107080366709, 1.000000000000000000 ) ) 
 REPRESENTATION_ITEM ( '' )  );
#9317=VERTEX_POINT ( 'NONE', #1669 ) ;
#9318=CARTESIAN_POINT ( 'NONE',  ( -1.348357406114881751, 47.70104341108812918, 85.28382765310961133 ) ) ;
#9319=ORIENTED_EDGE ( 'NONE', *, *, #20151, .T. ) ;
#9337=ORIENTED_EDGE ( 'NONE', *, *, #6382, .T. ) ;
#9352=ORIENTED_EDGE ( 'NONE', *, *, #16117, .T. ) ;
#9359=CARTESIAN_POINT ( 'NONE',  ( 0.5221537403065118488, 48.16218137147969003, 45.55433879953100273 ) ) ;
#9379=DIRECTION ( 'NONE',  ( -1.779391786395883536E-16, -5.922860397471806844E-17, 1.000000000000000000 ) ) ;
#9381=ADVANCED_FACE ( 'NONE', ( #11468 ), #17938, .T. ) ;
#9427=DIRECTION ( 'NONE',  ( -2.267473790562806355E-16, 5.922860397471811774E-17, -1.000000000000000000 ) ) ;
#9428=( BOUNDED_CURVE ( )  B_SPLINE_CURVE ( 3, ( #17065, #10488, #2063, #7155 ),
 .UNSPECIFIED., .F., .F. ) 
 B_SPLINE_CURVE_WITH_KNOTS ( ( 4, 4 ),
 ( 1.230959417340773854, 1.276280841686759260 ),
 .UNSPECIFIED. ) 
 CURVE ( )  GEOMETRIC_REPRESENTATION_ITEM ( )  RATIONAL_B_SPLINE_CURVE ( ( 1.000000000000000000, 0.9998288380325437430, 0.9998288380325437430, 1.000000000000000000 ) ) 
 REPRESENTATION_ITEM ( '' )  );
#9442=ORIENTED_EDGE ( 'NONE', *, *, #13144, .T. ) ;
#9461=VECTOR ( 'NONE', #4435, 1000.000000000000114 ) ;
#9462=CARTESIAN_POINT ( 'NONE',  ( -1.477846259693495146, 50.16218137147969713, 82.55433879953099563 ) ) ;
#9477=CARTESIAN_POINT ( 'NONE',  ( 2.122153740306512937, 47.82824192744436687, 53.55433879953100273 ) ) ;
#9484=CARTESIAN_POINT ( 'NONE',  ( 0.5221537403065048544, 44.16218137147969713, 82.55433879953099563 ) ) ;
#9502=PLANE ( 'NONE',  #5786 ) ;
#9512=ORIENTED_EDGE ( 'NONE', *, *, #15237, .F. ) ;
#9516=PLANE ( 'NONE',  #20708 ) ;
#9534=EDGE_CURVE ( 'NONE', #16835, #6239, #18808, .T. ) ;
#9539=CARTESIAN_POINT ( 'NONE',  ( 0.5221537403065114047, 44.16218137147969713, 45.55433879953100273 ) ) ;
#9541=LINE ( 'NONE', #18027, #11558 ) ;
#9543=ORIENTED_EDGE ( 'NONE', *, *, #20540, .F. ) ;
#9575=DIRECTION ( 'NONE',  ( -1.779391786395883536E-16, -5.922860397471806844E-17, 1.000000000000000000 ) ) ;
#9586=VECTOR ( 'NONE', #2202, 999.9999999999998863 ) ;
#9589=DIRECTION ( 'NONE',  ( 0.000000000000000000, 1.000000000000000000, 0.000000000000000000 ) ) ;
#9590=CARTESIAN_POINT ( 'NONE',  ( 0.5221537403065105165, 44.16218137147969713, 50.55433879953100273 ) ) ;
#9607=ORIENTED_EDGE ( 'NONE', *, *, #10649, .F. ) ;
#9609=EDGE_CURVE ( 'NONE', #12054, #10195, #14067, .T. ) ;
#9619=CARTESIAN_POINT ( 'NONE',  ( 0.5221537403065042993, 44.16218137147969713, 85.55433879953100984 ) ) ;
#9620=EDGE_CURVE ( 'NONE', #6883, #6753, #3952, .T. ) ;
#9623=CARTESIAN_POINT ( 'NONE',  ( -0.07555581626192756084, 50.25084051303456079, 77.06567965797611919 ) ) ;
#9625=ORIENTED_EDGE ( 'NONE', *, *, #4775, .T. ) ;
#9673=DIRECTION ( 'NONE',  ( -1.111814006898795283E-16, 5.922860397471810542E-17, -1.000000000000000000 ) ) ;
#9724=FACE_OUTER_BOUND ( 'NONE', #4415, .T. ) ;
#9742=DIRECTION ( 'NONE',  ( -1.084202172485505420E-16, -1.000000000000000000, 0.000000000000000000 ) ) ;
#9770=ADVANCED_FACE ( 'NONE', ( #6488 ), #12995, .T. ) ;
#9775=DIRECTION ( 'NONE',  ( 1.779391786395883536E-16, 5.922860397471806844E-17, -1.000000000000000000 ) ) ;
#9783=DIRECTION ( 'NONE',  ( -1.000000000000000000, 1.110223024625156540E-16, -1.779391786395883043E-16 ) ) ;
#9784=CARTESIAN_POINT ( 'NONE',  ( 2.522153740306510628, 47.62628298661744708, 53.15433879953100416 ) ) ;
#9790=CARTESIAN_POINT ( 'NONE',  ( 2.259191861956057146, 47.76843358786783966, 69.41730067788145675 ) ) ;
#9806=ORIENTED_EDGE ( 'NONE', *, *, #1429, .F. ) ;
#9815=ORIENTED_EDGE ( 'NONE', *, *, #810, .F. ) ;
#9818=CARTESIAN_POINT ( 'NONE',  ( 2.522153740306506631, 50.16218137147969713, 77.15433879953100416 ) ) ;
#9822=ORIENTED_EDGE ( 'NONE', *, *, #831, .T. ) ;
#9833=CARTESIAN_POINT ( 'NONE',  ( -1.348357406114871315, 47.70104341108813628, 61.28382765310961844 ) ) ;
#9845=FACE_OUTER_BOUND ( 'NONE', #14013, .T. ) ;
#9870=CARTESIAN_POINT ( 'NONE',  ( -1.477846259693494257, 49.16218137147969003, 74.55433879953100984 ) ) ;
#9885=PLANE ( 'NONE',  #20346 ) ;
#9892=EDGE_CURVE ( 'NONE', #20138, #13218, #15834, .T. ) ;
#9905=DIRECTION ( 'NONE',  ( -1.110223024625156540E-16, -1.000000000000000000, -5.922860397471808077E-17 ) ) ;
#9929=ORIENTED_EDGE ( 'NONE', *, *, #6614, .T. ) ;
#9935=ORIENTED_EDGE ( 'NONE', *, *, #14019, .F. ) ;
#9938=ORIENTED_EDGE ( 'NONE', *, *, #12225, .F. ) ;
#9952=AXIS2_PLACEMENT_3D ( 'NONE', #21032, #6468, #12973 ) ;
#9955=CARTESIAN_POINT ( 'NONE',  ( 2.122153740306507608, 50.16218137147969713, 85.55433879953100984 ) ) ;
#9956=VECTOR ( 'NONE', #12554, 1000.000000000000000 ) ;
#9961=CARTESIAN_POINT ( 'NONE',  ( -1.477846259693490705, 49.81903562097208038, 61.15433879953099705 ) ) ;
#9963=DIRECTION ( 'NONE',  ( -1.779391786395883536E-16, -5.922860397471806844E-17, 1.000000000000000000 ) ) ;
#9968=EDGE_CURVE ( 'NONE', #20977, #5606, #4249, .T. ) ;
#9981=ORIENTED_EDGE ( 'NONE', *, *, #20288, .T. ) ;
#9999=CIRCLE ( 'NONE', #1833, 3.999999999999996447 ) ;
#10016=CARTESIAN_POINT ( 'NONE',  ( 2.522153740306509739, 50.16218137147969713, 59.55433879953099563 ) ) ;
#10019=ORIENTED_EDGE ( 'NONE', *, *, #2496, .T. ) ;
#10021=DIRECTION ( 'NONE',  ( -4.731737692062757470E-17, 0.7071067811865512365, 0.7071067811865439090 ) ) ;
#10037=CARTESIAN_POINT ( 'NONE',  ( 1.771153339986189845, 40.36218137147969998, 46.35433879953098568 ) ) ;
#10042=EDGE_CURVE ( 'NONE', #14796, #20391, #2114, .T. ) ;
#10049=EDGE_LOOP ( 'NONE', ( #3319, #14968, #12915, #6224, #8433 ) ) ;
#10055=DIRECTION ( 'NONE',  ( -1.779391786395883536E-16, -5.922860397471806844E-17, 1.000000000000000000 ) ) ;
#10086=EDGE_LOOP ( 'NONE', ( #11356, #399, #12052, #17516, #12548 ) ) ;
#10098=ORIENTED_EDGE ( 'NONE', *, *, #7551, .F. ) ;
#10100=EDGE_CURVE ( 'NONE', #16102, #4527, #3592, .T. ) ;
#10101=DIRECTION ( 'NONE',  ( -1.110223024625156540E-16, -1.000000000000000000, -5.922860397471808077E-17 ) ) ;
#10120=PLANE ( 'NONE',  #19448 ) ;
#10130=LINE ( 'NONE', #16610, #3309 ) ;
#10136=EDGE_CURVE ( 'NONE', #880, #19954, #13591, .T. ) ;
#10143=VERTEX_POINT ( 'NONE', #16690 ) ;
#10147=ORIENTED_EDGE ( 'NONE', *, *, #4140, .T. ) ;
#10182=DIRECTION ( 'NONE',  ( -1.000000000000000000, 0.000000000000000000, 0.000000000000000000 ) ) ;
#10188=EDGE_CURVE ( 'NONE', #880, #6384, #20951, .T. ) ;
#10195=VERTEX_POINT ( 'NONE', #9249 ) ;
#10198=AXIS2_PLACEMENT_3D ( 'NONE', #19974, #10337, #15323 ) ;
#10202=DIRECTION ( 'NONE',  ( -0.7071067811865535679, 1.203855704449247279E-16, -0.7071067811865414665 ) ) ;
#10211=CARTESIAN_POINT ( 'NONE',  ( 27.27315414062681853, 40.36218137147969287, 87.85433879953103542 ) ) ;
#10218=CIRCLE ( 'NONE', #6105, 4.000000000000000000 ) ;
#10236=ORIENTED_EDGE ( 'NONE', *, *, #3514, .T. ) ;
#10237=AXIS2_PLACEMENT_3D ( 'NONE', #9484, #15971, #12872 ) ;
#10253=CARTESIAN_POINT ( 'NONE',  ( 0.5221537403065104055, 40.36218137147969998, 46.15433879953098284 ) ) ;
#10268=ORIENTED_EDGE ( 'NONE', *, *, #13092, .T. ) ;
#10285=VERTEX_POINT ( 'NONE', #7954 ) ;
#10293=ORIENTED_EDGE ( 'NONE', *, *, #9073, .F. ) ;
#10302=DIRECTION ( 'NONE',  ( -1.110223024625156540E-16, -1.000000000000000000, -5.922860397471808077E-17 ) ) ;
#10305=DIRECTION ( 'NONE',  ( -1.000000000000000000, 0.000000000000000000, 0.000000000000000000 ) ) ;
#10306=VECTOR ( 'NONE', #7135, 1000.000000000000000 ) ;
#10313=CARTESIAN_POINT ( 'NONE',  ( -1.477846259693499364, 49.81903562097207327, 83.21119304902337888 ) ) ;
#10318=ORIENTED_EDGE ( 'NONE', *, *, #5060, .F. ) ;
#10334=CARTESIAN_POINT ( 'NONE',  ( 2.522153740306509739, 49.16218137147969003, 58.55433879953100984 ) ) ;
#10337=DIRECTION ( 'NONE',  ( -1.779391786395883536E-16, -5.922860397471806844E-17, 1.000000000000000000 ) ) ;
#10344=FACE_OUTER_BOUND ( 'NONE', #8867, .T. ) ;
#10347=ORIENTED_EDGE ( 'NONE', *, *, #18419, .F. ) ;
#10353=DIRECTION ( 'NONE',  ( -1.000000000000000000, 1.110223024625156540E-16, -1.779391786395883043E-16 ) ) ;
#10354=DIRECTION ( 'NONE',  ( -3.211742425186504723E-16, 5.922860397471811774E-17, -1.000000000000000000 ) ) ;
#10374=FACE_OUTER_BOUND ( 'NONE', #3323, .T. ) ;
#10397=EDGE_LOOP ( 'NONE', ( #18797, #18019, #11532, #9352 ) ) ;
#10439=EDGE_CURVE ( 'NONE', #20391, #14499, #8627, .T. ) ;
#10442=ADVANCED_FACE ( 'NONE', ( #16874 ), #10508, .T. ) ;
#10450=DIRECTION ( 'NONE',  ( -1.779391786395883536E-16, -5.922860397471806844E-17, 1.000000000000000000 ) ) ;
#10451=ORIENTED_EDGE ( 'NONE', *, *, #13144, .F. ) ;
#10461=CARTESIAN_POINT ( 'NONE',  ( 28.52215374030649642, 44.16218137147969003, 87.85433879953103542 ) ) ;
#10484=LINE ( 'NONE', #8982, #5369 ) ;
#10485=LINE ( 'NONE', #7152, #10790 ) ;
#10488=CARTESIAN_POINT ( 'NONE',  ( -1.392380047608623439, 49.84925249003585179, 53.23980501161587853 ) ) ;
#10508=PLANE ( 'NONE',  #2946 ) ;
#10509=CARTESIAN_POINT ( 'NONE',  ( 2.263811127080450625, 49.90383875825364157, 85.41268141275705261 ) ) ;
#10519=FACE_OUTER_BOUND ( 'NONE', #10397, .T. ) ;
#10520=CARTESIAN_POINT ( 'NONE',  ( -0.7268458593731683681, 40.36218137147969998, 46.35433879953098568 ) ) ;
#10522=ORIENTED_EDGE ( 'NONE', *, *, #10042, .T. ) ;
#10532=DIRECTION ( 'NONE',  ( 1.110223024625156540E-16, 1.000000000000000000, 5.922860397471808077E-17 ) ) ;
#10546=CARTESIAN_POINT ( 'NONE',  ( -1.477846259693502917, 47.62628298661744708, 77.15433879953100416 ) ) ;
#10547=VECTOR ( 'NONE', #19194, 1000.000000000000000 ) ;
#10556=VECTOR ( 'NONE', #5420, 1000.000000000000114 ) ;
#10564=CARTESIAN_POINT ( 'NONE',  ( -1.477846259693486486, 49.81903562097206617, 123.5543387995310098 ) ) ;
#10568=CARTESIAN_POINT ( 'NONE',  ( 2.263811127080455954, 49.90383875825364157, 53.41268141275705972 ) ) ;
#10609=PRODUCT ( 'Shackle', 'Shackle', '', ( #2407 ) ) ;
#10610=ORIENTED_EDGE ( 'NONE', *, *, #18862, .F. ) ;
#10633=AXIS2_PLACEMENT_3D ( 'NONE', #6499, #4586, #6192 ) ;
#10634=CARTESIAN_POINT ( 'NONE',  ( 2.122153740306512937, 50.16218137147969713, 53.55433879953100273 ) ) ;
#10638=ORIENTED_EDGE ( 'NONE', *, *, #16944, .F. ) ;
#10641=CARTESIAN_POINT ( 'NONE',  ( 2.522153740306511960, 47.62628298661745418, 45.55433879953100273 ) ) ;
#10644=CARTESIAN_POINT ( 'NONE',  ( -1.477846259693490705, 49.81903562097208038, 61.15433879953099705 ) ) ;
#10649=EDGE_CURVE ( 'NONE', #7228, #14869, #18441, .T. ) ;
#10654=DIRECTION ( 'NONE',  ( -1.111814006898795283E-16, 5.922860397471810542E-17, -1.000000000000000000 ) ) ;
#10660=EDGE_CURVE ( 'NONE', #12054, #11891, #10485, .T. ) ;
#10668=CARTESIAN_POINT ( 'NONE',  ( 0.5221537403065064087, 48.16218137147969003, 77.55433879953099563 ) ) ;
#10674=DIRECTION ( 'NONE',  ( 1.000000000000000000, -1.110223024625156540E-16, 1.779391786395883043E-16 ) ) ;
#10695=CARTESIAN_POINT ( 'NONE',  ( -1.477846259693498920, 49.81903562097206617, 75.21119304902337888 ) ) ;
#10710=EDGE_CURVE ( 'NONE', #8000, #10285, #19713, .T. ) ;
#10727=ORIENTED_EDGE ( 'NONE', *, *, #3536, .T. ) ;
#10732=EDGE_CURVE ( 'NONE', #8473, #5980, #1102, .T. ) ;
#10742=ORIENTED_EDGE ( 'NONE', *, *, #12095, .T. ) ;
#10745=FACE_OUTER_BOUND ( 'NONE', #12425, .T. ) ;
#10756=CARTESIAN_POINT ( 'NONE',  ( -1.219503646467429814, 49.90383875825364157, 53.41268141275706682 ) ) ;
#10772=DIRECTION ( 'NONE',  ( -1.000000000000000000, 1.110223024625156540E-16, 6.575695984913707633E-33 ) ) ;
#10785=CARTESIAN_POINT ( 'NONE',  ( 2.122153740306508496, 47.82824192744436687, 77.55433879953099563 ) ) ;
#10790=VECTOR ( 'NONE', #5131, 1000.000000000000000 ) ;
#10803=ORIENTED_EDGE ( 'NONE', *, *, #12185, .F. ) ;
#10810=DIRECTION ( 'NONE',  ( 1.000000000000000000, 0.000000000000000000, 0.000000000000000000 ) ) ;
#10820=DIRECTION ( 'NONE',  ( -1.000000000000000000, 1.110223024625156540E-16, -1.779391786395883043E-16 ) ) ;
#10822=ORIENTED_EDGE ( 'NONE', *, *, #7074, .T. ) ;
#10835=EDGE_LOOP ( 'NONE', ( #13653, #11763, #1951, #11637, #7632, #18716 ) ) ;
#10842=ORIENTED_EDGE ( 'NONE', *, *, #7390, .T. ) ;
#10851=EDGE_CURVE ( 'NONE', #13249, #18186, #17565, .T. ) ;
#10865=DIRECTION ( 'NONE',  ( -1.000000000000000000, 1.110223024625156540E-16, -1.779391786395883043E-16 ) ) ;
#10871=PLANE ( 'NONE',  #8752 ) ;
#10876=CARTESIAN_POINT ( 'NONE',  ( -1.477846259693493369, 50.16218137147969713, 77.55433879953099563 ) ) ;
#10878=VECTOR ( 'NONE', #12957, 1000.000000000000000 ) ;
#10887=DIRECTION ( 'NONE',  ( -4.142850521348543581E-16, 5.922860397471813007E-17, -1.000000000000000000 ) ) ;
#10890=FACE_OUTER_BOUND ( 'NONE', #8332, .T. ) ;
#10900=ORIENTED_EDGE ( 'NONE', *, *, #2328, .F. ) ;
#10911=ORIENTED_EDGE ( 'NONE', *, *, #16944, .T. ) ;
#10918=DIRECTION ( 'NONE',  ( -3.211742425186504723E-16, 5.922860397471811774E-17, -1.000000000000000000 ) ) ;
#10919=EDGE_LOOP ( 'NONE', ( #17581, #14105, #20306, #9319, #10842 ) ) ;
#10922=ADVANCED_FACE ( 'NONE', ( #9079 ), #665, .F. ) ;
#10923=VERTEX_POINT ( 'NONE', #20447 ) ;
#10934=EDGE_LOOP ( 'NONE', ( #3891, #7413, #15133, #3224, #2867 ) ) ;
#10946=CIRCLE ( 'NONE', #3448, 3.999999999999996447 ) ;
#10954=CARTESIAN_POINT ( 'NONE',  ( -1.477846259693489372, 50.16218137147969713, 50.55433879953100273 ) ) ;
#10956=DIRECTION ( 'NONE',  ( 0.5773502691896226224, 0.5773502691896224004, -0.5773502691896322814 ) ) ;
#10965=CARTESIAN_POINT ( 'NONE',  ( 2.522153740306511516, 50.16218137147969713, 51.55433879953100273 ) ) ;
#10966=CARTESIAN_POINT ( 'NONE',  ( -1.477846259693492481, 49.81903562097207327, 69.15433879953098995 ) ) ;
#10973=MANIFOLD_SOLID_BREP ( 'Stock-MAS-160-1', #12560 ) ;
#10977=CARTESIAN_POINT ( 'NONE',  ( -1.077846259693481246, 47.82824192744437397, 69.55433879953100984 ) ) ;
#10981=CARTESIAN_POINT ( 'NONE',  ( 2.522153740306507963, 50.16218137147969713, 69.15433879953098995 ) ) ;
#10982=CARTESIAN_POINT ( 'NONE',  ( 14.52215374030650175, 44.16218137147969003, 105.5543387995309956 ) ) ;
#10985=ORIENTED_EDGE ( 'NONE', *, *, #18068, .T. ) ;
#10989=DIRECTION ( 'NONE',  ( -1.779391786395883536E-16, -5.922860397471806844E-17, 1.000000000000000000 ) ) ;
#11011=ORIENTED_EDGE ( 'NONE', *, *, #18213, .T. ) ;
#11058=SHAPE_REPRESENTATION_RELATIONSHIP ( 'NONE' , 'NONE' ,  #209, #11387 ) ;
#11062=FACE_OUTER_BOUND ( 'NONE', #12933, .T. ) ;
#11072=ORIENTED_EDGE ( 'NONE', *, *, #13273, .F. ) ;
#11088=LINE ( 'NONE', #14368, #11279 ) ;
#11112=DIRECTION ( 'NONE',  ( -1.000000000000000000, 1.110223024625156540E-16, -1.779391786395883043E-16 ) ) ;
#11118=ORIENTED_EDGE ( 'NONE', *, *, #7074, .F. ) ;
#11122=CARTESIAN_POINT ( 'NONE',  ( 2.522153740306498193, 49.81903562097208038, 123.5543387995310098 ) ) ;
#11123=ORIENTED_EDGE ( 'NONE', *, *, #9534, .F. ) ;
#11136=VERTEX_POINT ( 'NONE', #4143 ) ;
#11149=DIRECTION ( 'NONE',  ( -1.084202172485505420E-16, -1.000000000000000000, 0.000000000000000000 ) ) ;
#11161=CARTESIAN_POINT ( 'NONE',  ( 2.122153740306511605, 50.16218137147969713, 61.55433879953100273 ) ) ;
#11167=DIRECTION ( 'NONE',  ( 0.5773502691896259531, 0.5773502691896257311, -0.5773502691896256200 ) ) ;
#11172=ORIENTED_EDGE ( 'NONE', *, *, #6139, .F. ) ;
#11183=DIRECTION ( 'NONE',  ( -1.779391786395883536E-16, -5.922860397471806844E-17, 1.000000000000000000 ) ) ;
#11194=VECTOR ( 'NONE', #15748, 1000.000000000000114 ) ;
#11209=EDGE_CURVE ( 'NONE', #2898, #5606, #15334, .T. ) ;
#11213=ADVANCED_FACE ( 'NONE', ( #747 ), #15120, .T. ) ;
#11243=ORIENTED_EDGE ( 'NONE', *, *, #2328, .T. ) ;
#11246=AXIS2_PLACEMENT_3D ( 'NONE', #10876, #12359, #20627 ) ;
#11272=CARTESIAN_POINT ( 'NONE',  ( 2.122153740306512937, 49.76218137147969856, 53.55433879953100273 ) ) ;
#11275=DIRECTION ( 'NONE',  ( -1.110223024625156540E-16, -1.000000000000000000, -5.922860397471808077E-17 ) ) ;
#11278=CARTESIAN_POINT ( 'NONE',  ( 0.5221537403065118488, 48.16218137147969003, 45.55433879953100273 ) ) ;
#11279=VECTOR ( 'NONE', #18943, 1000.000000000000000 ) ;
#11281=ORIENTED_EDGE ( 'NONE', *, *, #15920, .F. ) ;
#11286=DIRECTION ( 'NONE',  ( -1.779391786395883536E-16, -5.922860397471806844E-17, 1.000000000000000000 ) ) ;
#11292=VECTOR ( 'NONE', #9575, 1000.000000000000000 ) ;
#11317=ADVANCED_FACE ( 'NONE', ( #6053 ), #10871, .F. ) ;
#11338=ORIENTED_EDGE ( 'NONE', *, *, #10042, .F. ) ;
#11346=DIRECTION ( 'NONE',  ( -1.000000000000000000, 0.000000000000000000, 0.000000000000000000 ) ) ;
#11348=CARTESIAN_POINT ( 'NONE',  ( -0.8111795930268231869, 49.49551470481303284, 53.82100546619766845 ) ) ;
#11356=ORIENTED_EDGE ( 'NONE', *, *, #6602, .F. ) ;
#11368=VECTOR ( 'NONE', #16304, 1000.000000000000000 ) ;
#11384=CARTESIAN_POINT ( 'NONE',  ( 2.259191861956068692, 47.76843358786783966, 53.41730067788145675 ) ) ;
#11387=ADVANCED_BREP_SHAPE_REPRESENTATION ( '', ( #10973, #18366 ), #4082 ) ;
#11389=CARTESIAN_POINT ( 'NONE',  ( 0.5221537403065064087, 48.16218137147969003, 61.55433879953100273 ) ) ;
#11399=CARTESIAN_POINT ( 'NONE',  ( 2.522153740306505298, 50.16218137147969713, 85.15433879953098995 ) ) ;
#11406=VERTEX_POINT ( 'NONE', #11389 ) ;
#11412=ORIENTED_EDGE ( 'NONE', *, *, #18213, .F. ) ;
#11418=PLANE ( 'NONE',  #10633 ) ;
#11424=ORIENTED_EDGE ( 'NONE', *, *, #9892, .F. ) ;
#11432=ADVANCED_FACE ( 'NONE', ( #1903 ), #14873, .F. ) ;
#11437=LINE ( 'NONE', #17909, #4189 ) ;
#11452=CARTESIAN_POINT ( 'NONE',  ( 0.5221537403065048544, 44.16218137147969713, 82.55433879953099563 ) ) ;
#11455=EDGE_CURVE ( 'NONE', #19954, #16819, #14771, .T. ) ;
#11465=LINE ( 'NONE', #11568, #7457 ) ;
#11468=FACE_OUTER_BOUND ( 'NONE', #15513, .T. ) ;
#11509=CARTESIAN_POINT ( 'NONE',  ( 2.522153740306504854, 49.81903562097208038, 85.15433879953098995 ) ) ;
#11528=ORIENTED_EDGE ( 'NONE', *, *, #20137, .T. ) ;
#11532=ORIENTED_EDGE ( 'NONE', *, *, #10851, .T. ) ;
#11536=CARTESIAN_POINT ( 'NONE',  ( 2.522153740306507519, 49.81903562097208038, 69.15433879953098995 ) ) ;
#11551=DIRECTION ( 'NONE',  ( 0.000000000000000000, 1.000000000000000000, 0.000000000000000000 ) ) ;
#11558=VECTOR ( 'NONE', #6314, 1000.000000000000000 ) ;
#11568=CARTESIAN_POINT ( 'NONE',  ( -1.477846259693499809, 47.62628298661744708, 45.55433879953100273 ) ) ;
#11600=ADVANCED_FACE ( 'NONE', ( #4115 ), #13913, .F. ) ;
#11613=AXIS2_PLACEMENT_3D ( 'NONE', #7571, #14053, #2782 ) ;
#11620=VECTOR ( 'NONE', #9783, 1000.000000000000000 ) ;
#11637=ORIENTED_EDGE ( 'NONE', *, *, #19759, .T. ) ;
#11645=CARTESIAN_POINT ( 'NONE',  ( -1.477846259693495590, 47.62628298661744708, 61.15433879953099705 ) ) ;
#11666=LINE ( 'NONE', #258, #3114 ) ;
#11696=ORIENTED_EDGE ( 'NONE', *, *, #16117, .F. ) ;
#11706=EDGE_CURVE ( 'NONE', #15567, #16100, #1470, .T. ) ;
#11711=VERTEX_POINT ( 'NONE', #6761 ) ;
#11728=APPLICATION_CONTEXT ( 'automotive_design' ) ;
#11737=EDGE_CURVE ( 'NONE', #19622, #12696, #584, .T. ) ;
#11763=ORIENTED_EDGE ( 'NONE', *, *, #10136, .F. ) ;
#11788=DIRECTION ( 'NONE',  ( 1.000000000000000000, -1.110223024625156540E-16, 1.779391786395883043E-16 ) ) ;
#11789=LINE ( 'NONE', #8491, #1074 ) ;
#11804=DIRECTION ( 'NONE',  ( -1.084202172485505420E-16, -1.000000000000000000, 0.000000000000000000 ) ) ;
#11806=VECTOR ( 'NONE', #4867, 1000.000000000000114 ) ;
#11813=LINE ( 'NONE', #13609, #9238 ) ;
#11819=ORIENTED_EDGE ( 'NONE', *, *, #6591, .F. ) ;
#11824=LINE ( 'NONE', #18299, #1796 ) ;
#11849=EDGE_CURVE ( 'NONE', #14474, #880, #1935, .T. ) ;
#11853=EDGE_CURVE ( 'NONE', #14499, #347, #13329, .T. ) ;
#11860=CIRCLE ( 'NONE', #5381, 3.999999999999996447 ) ;
#11863=LINE ( 'NONE', #5349, #18677 ) ;
#11865=VERTEX_POINT ( 'NONE', #11947 ) ;
#11871=DIRECTION ( 'NONE',  ( -1.000000000000000000, 0.000000000000000000, 0.000000000000000000 ) ) ;
#11890=CARTESIAN_POINT ( 'NONE',  ( 2.350558581813038117, 49.87752504164859602, 69.32593395802446423 ) ) ;
#11891=VERTEX_POINT ( 'NONE', #18425 ) ;
#11892=ORIENTED_EDGE ( 'NONE', *, *, #14549, .F. ) ;
#11900=EDGE_LOOP ( 'NONE', ( #17723, #3994, #3864, #10268, #7524, #3351 ) ) ;
#11919=DIRECTION ( 'NONE',  ( -1.779391786395883536E-16, -5.922860397471806844E-17, 1.000000000000000000 ) ) ;
#11929=CARTESIAN_POINT ( 'NONE',  ( 28.52215374030649642, 44.16218137147969003, 87.85433879953103542 ) ) ;
#11939=LINE ( 'NONE', #642, #10556 ) ;
#11947=CARTESIAN_POINT ( 'NONE',  ( 2.122153740306508496, 47.82824192744436687, 77.55433879953099563 ) ) ;
#11974=EDGE_CURVE ( 'NONE', #16856, #6568, #14091, .T. ) ;
#11984=VERTEX_POINT ( 'NONE', #16834 ) ;
#11987=LINE ( 'NONE', #18783, #15631 ) ;
#11988=EDGE_CURVE ( 'NONE', #16102, #4359, #2252, .T. ) ;
#11992=ORIENTED_EDGE ( 'NONE', *, *, #19596, .F. ) ;
#12001=CARTESIAN_POINT ( 'NONE',  ( -1.477846259693492481, 50.16218137147969713, 66.55433879953099563 ) ) ;
#12004=CIRCLE ( 'NONE', #2438, 17.99999999999999645 ) ;
#12005=ORIENTED_EDGE ( 'NONE', *, *, #5435, .T. ) ;
#12006=VERTEX_POINT ( 'NONE', #18634 ) ;
#12017=CARTESIAN_POINT ( 'NONE',  ( 0.5221537403065091842, 44.16218137147969713, 58.55433879953100984 ) ) ;
#12037=CARTESIAN_POINT ( 'NONE',  ( -1.477846259693495590, 47.62628298661744708, 61.15433879953099705 ) ) ;
#12043=ORIENTED_EDGE ( 'NONE', *, *, #17712, .T. ) ;
#12052=ORIENTED_EDGE ( 'NONE', *, *, #1932, .T. ) ;
#12054=VERTEX_POINT ( 'NONE', #762 ) ;
#12088=CARTESIAN_POINT ( 'NONE',  ( 28.94982316289697621, 40.36218137147969287, 87.65433879953101837 ) ) ;
#12095=EDGE_CURVE ( 'NONE', #15360, #20516, #12632, .T. ) ;
#12098=PLANE ( 'NONE',  #15720 ) ;
#12105=DIRECTION ( 'NONE',  ( 1.110223024625156540E-16, 1.000000000000000000, 5.922860397471808077E-17 ) ) ;
#12115=CARTESIAN_POINT ( 'NONE',  ( 2.522153740306505743, 50.16218137147969713, 82.55433879953099563 ) ) ;
#12131=PLANE ( 'NONE',  #1763 ) ;
#12143=CARTESIAN_POINT ( 'NONE',  ( -1.477846259693493369, 50.16218137147969713, 77.15433879953100416 ) ) ;
#12154=ORIENTED_EDGE ( 'NONE', *, *, #6626, .F. ) ;
#12167=AXIS2_PLACEMENT_3D ( 'NONE', #10981, #4459, #14142 ) ;
#12185=EDGE_CURVE ( 'NONE', #6294, #15169, #6691, .T. ) ;
#12207=LINE ( 'NONE', #9126, #9586 ) ;
#12219=FACE_OUTER_BOUND ( 'NONE', #13971, .T. ) ;
#12222=AXIS2_PLACEMENT_3D ( 'NONE', #20883, #12719, #11551 ) ;
#12225=EDGE_CURVE ( 'NONE', #4837, #140, #1822, .T. ) ;
#12230=AXIS2_PLACEMENT_3D ( 'NONE', #12017, #4112, #2313 ) ;
#12249=EDGE_CURVE ( 'NONE', #7189, #14664, #11813, .T. ) ;
#12261=VECTOR ( 'NONE', #14029, 1000.000000000000000 ) ;
#12265=ORIENTED_EDGE ( 'NONE', *, *, #3514, .F. ) ;
#12273=CARTESIAN_POINT ( 'NONE',  ( 1.215246153217546921, 50.28109722957945138, 75.67325465763076409 ) ) ;
#12275=ADVANCED_FACE ( 'NONE', ( #15326 ), #8938, .T. ) ;
#12304=CARTESIAN_POINT ( 'NONE',  ( 28.52215374030649642, 40.36218137147969287, 87.65433879953101837 ) ) ;
#12338=EDGE_CURVE ( 'NONE', #10285, #11136, #2650, .T. ) ;
#12344=CARTESIAN_POINT ( 'NONE',  ( -1.214884381343054987, 47.76843358786783256, 77.41730067788147096 ) ) ;
#12356=DIRECTION ( 'NONE',  ( 0.5773502691896259531, 0.5773502691896257311, -0.5773502691896256200 ) ) ;
#12357=CARTESIAN_POINT ( 'NONE',  ( -1.477846259693490705, 50.16218137147969713, 58.55433879953100984 ) ) ;
#12359=DIRECTION ( 'NONE',  ( 1.779391786395883536E-16, 5.922860397471805611E-17, -1.000000000000000000 ) ) ;
#12371=ORIENTED_EDGE ( 'NONE', *, *, #16723, .T. ) ;
#12425=EDGE_LOOP ( 'NONE', ( #16062, #3014, #10019, #10742, #5598 ) ) ;
#12440=CARTESIAN_POINT ( 'NONE',  ( 28.52215374030649642, 48.16218137147969003, 87.85433879953103542 ) ) ;
#12457=DIRECTION ( 'NONE',  ( 1.016439536705157818E-16, 1.000000000000000000, 0.000000000000000000 ) ) ;
#12472=STYLED_ITEM ( 'NONE', ( #19262 ), #10973 ) ;
#12484=CARTESIAN_POINT ( 'NONE',  ( 28.52215374030649642, 40.36218137147969287, 87.65433879953101837 ) ) ;
#12493=EDGE_CURVE ( 'NONE', #140, #14499, #11789, .T. ) ;
#12495=CARTESIAN_POINT ( 'NONE',  ( 0.5221537403065364957, 44.16218137147969003, 123.5543387995310098 ) ) ;
#12510=EDGE_CURVE ( 'NONE', #14796, #8473, #18168, .T. ) ;
#12515=VERTEX_POINT ( 'NONE', #16262 ) ;
#12517=EDGE_LOOP ( 'NONE', ( #11412, #4506, #4002, #17701, #12043 ) ) ;
#12534=EDGE_CURVE ( 'NONE', #8576, #15405, #12004, .T. ) ;
#12548=ORIENTED_EDGE ( 'NONE', *, *, #11974, .F. ) ;
#12553=DIRECTION ( 'NONE',  ( -1.000000000000000000, 1.110223024625156540E-16, -1.779391786395883043E-16 ) ) ;
#12554=DIRECTION ( 'NONE',  ( -1.000000000000000000, 1.110223024625156540E-16, -1.779391786395883043E-16 ) ) ;
#12560=CLOSED_SHELL ( 'NONE', ( #7538, #20788, #18971, #17830, #802, #644, #6897, #14470, #14126, #9381, #3123, #7920, #18432, #3062, #6738, #17947, #11600, #3089, #2484, #13524, #10922, #12275, #8835, #10442, #7024, #2444, #2888, #19016, #11213, #3128, #13010, #9770, #9064, #380, #11432, #6353, #15373, #3677, #2053, #14336, #5009, #17304, #9118, #19511, #20777, #9192, #11317, #13788, #9279, #19851, #16009, #20088, #18581, #118, #14670, #18973, #809, #145, #14812, #1391 ) ) ;
#12576=CONICAL_SURFACE ( 'NONE', #12905, 4.000000000000003553, 0.7853981633974460586 ) ;
#12595=ORIENTED_EDGE ( 'NONE', *, *, #15896, .F. ) ;
#12596=CARTESIAN_POINT ( 'NONE',  ( 0.5221537403065064087, 50.16218137147969713, 77.15433879953100416 ) ) ;
#12602=ORIENTED_EDGE ( 'NONE', *, *, #14809, .T. ) ;
#12608=EDGE_LOOP ( 'NONE', ( #14628, #11696, #5821, #8798 ) ) ;
#12612=ORIENTED_EDGE ( 'NONE', *, *, #11849, .F. ) ;
#12624=ORIENTED_EDGE ( 'NONE', *, *, #1024, .F. ) ;
#12632=CIRCLE ( 'NONE', #15743, 3.999999999999996447 ) ;
#12643=CARTESIAN_POINT ( 'NONE',  ( -1.306251101200022857, 49.87752504164858891, 61.32593395802449265 ) ) ;
#12647=DIRECTION ( 'NONE',  ( 0.000000000000000000, 0.000000000000000000, 1.000000000000000000 ) ) ;
#12650=CARTESIAN_POINT ( 'NONE',  ( -1.477846259693506914, 47.62628298661743997, 85.15433879953098995 ) ) ;
#12660=ORIENTED_EDGE ( 'NONE', *, *, #17707, .F. ) ;
#12663=CARTESIAN_POINT ( 'NONE',  ( -1.477846259693499364, 47.62628298661744708, 69.15433879953098995 ) ) ;
#12671=DIRECTION ( 'NONE',  ( 1.084202172485505420E-16, 1.000000000000000000, 0.000000000000000000 ) ) ;
#12674=AXIS2_PLACEMENT_3D ( 'NONE', #13149, #8466, #14949 ) ;
#12684=CARTESIAN_POINT ( 'NONE',  ( 2.522153740306508407, 50.16218137147969713, 67.55433879953099563 ) ) ;
#12696=VERTEX_POINT ( 'NONE', #10520 ) ;
#12698=VERTEX_POINT ( 'NONE', #10313 ) ;
#12708=EDGE_CURVE ( 'NONE', #12698, #3704, #17103, .T. ) ;
#12713=ORIENTED_EDGE ( 'NONE', *, *, #4930, .F. ) ;
#12719=DIRECTION ( 'NONE',  ( -1.779391786395883536E-16, -5.922860397471806844E-17, 1.000000000000000000 ) ) ;
#12729=EDGE_CURVE ( 'NONE', #13088, #15854, #12207, .T. ) ;
#12750=CARTESIAN_POINT ( 'NONE',  ( -1.477846259693492037, 50.16218137147969713, 69.15433879953098995 ) ) ;
#12766=CARTESIAN_POINT ( 'NONE',  ( -1.477846259693506470, 47.62628298661743997, 82.55433879953099563 ) ) ;
#12784=DIRECTION ( 'NONE',  ( 1.000000000000000000, -1.110223024625156417E-16, -1.111814006898795283E-16 ) ) ;
#12795=VECTOR ( 'NONE', #14376, 1000.000000000000114 ) ;
#12805=LINE ( 'NONE', #1853, #761 ) ;
#12809=ORIENTED_EDGE ( 'NONE', *, *, #6382, .F. ) ;
#12815=CARTESIAN_POINT ( 'NONE',  ( 0.5221537403065118488, 48.16218137147969003, 45.55433879953100273 ) ) ;
#12825=CARTESIAN_POINT ( 'NONE',  ( 28.52215374030649642, 40.96218137147970850, 87.05433879953100984 ) ) ;
#12830=AXIS2_PLACEMENT_3D ( 'NONE', #20702, #18913, #14022 ) ;
#12836=( BOUNDED_CURVE ( )  B_SPLINE_CURVE ( 3, ( #5286, #8616, #9790, #3695 ),
 .UNSPECIFIED., .F., .F. ) 
 B_SPLINE_CURVE_WITH_KNOTS ( ( 4, 4 ),
 ( 4.188790204786389637, 4.300872134317204498 ),
 .UNSPECIFIED. ) 
 CURVE ( )  GEOMETRIC_REPRESENTATION_ITEM ( )  RATIONAL_B_SPLINE_CURVE ( ( 1.000000000000000000, 0.9989534107080366709, 0.9989534107080366709, 1.000000000000000000 ) ) 
 REPRESENTATION_ITEM ( '' )  );
#12843=DIRECTION ( 'NONE',  ( -1.110223024625156540E-16, -1.000000000000000000, -5.922860397471808077E-17 ) ) ;
#12850=CARTESIAN_POINT ( 'NONE',  ( 0.5221537403065061866, 44.16218137147969713, 74.55433879953100984 ) ) ;
#12853=CARTESIAN_POINT ( 'NONE',  ( -1.077846259693492126, 50.16218137147969713, 53.55433879953100273 ) ) ;
#12856=CARTESIAN_POINT ( 'NONE',  ( 2.392664886727894125, 47.70104341108812918, 53.28382765310963265 ) ) ;
#12872=DIRECTION ( 'NONE',  ( 1.084202172485505420E-16, 1.000000000000000000, 0.000000000000000000 ) ) ;
#12873=EDGE_CURVE ( 'NONE', #1135, #1015, #17990, .T. ) ;
#12878=EDGE_CURVE ( 'NONE', #9181, #12515, #16654, .T. ) ;
#12879=EDGE_CURVE ( 'NONE', #10143, #983, #11666, .T. ) ;
#12902=ORIENTED_EDGE ( 'NONE', *, *, #7514, .F. ) ;
#12905=AXIS2_PLACEMENT_3D ( 'NONE', #6733, #10055, #1955 ) ;
#12909=ORIENTED_EDGE ( 'NONE', *, *, #20743, .F. ) ;
#12915=ORIENTED_EDGE ( 'NONE', *, *, #13855, .T. ) ;
#12925=VECTOR ( 'NONE', #18090, 1000.000000000000000 ) ;
#12926=CARTESIAN_POINT ( 'NONE',  ( 0.5221537403065056315, 44.16218137147969713, 77.55433879953099563 ) ) ;
#12927=DIRECTION ( 'NONE',  ( -1.000000000000000000, 0.000000000000000000, 0.000000000000000000 ) ) ;
#12929=LINE ( 'NONE', #11348, #18767 ) ;
#12933=EDGE_LOOP ( 'NONE', ( #9822, #8430, #7626, #17320, #2831 ) ) ;
#12936=LINE ( 'NONE', #3153, #20762 ) ;
#12952=LINE ( 'NONE', #19433, #4069 ) ;
#12957=DIRECTION ( 'NONE',  ( -1.779391786395883536E-16, -5.922860397471806844E-17, 1.000000000000000000 ) ) ;
#12964=CARTESIAN_POINT ( 'NONE',  ( -1.477846259693489150, 50.16218137147969713, 53.55433879953100273 ) ) ;
#12966=( BOUNDED_CURVE ( )  B_SPLINE_CURVE ( 3, ( #4987, #1823, #14579, #11509 ),
 .UNSPECIFIED., .F., .F. ) 
 B_SPLINE_CURVE_WITH_KNOTS ( ( 4, 4 ),
 ( 5.006904465492823419, 5.052225889838807937 ),
 .UNSPECIFIED. ) 
 CURVE ( )  GEOMETRIC_REPRESENTATION_ITEM ( )  RATIONAL_B_SPLINE_CURVE ( ( 1.000000000000000000, 0.9998288380325438540, 0.9998288380325438540, 1.000000000000000000 ) ) 
 REPRESENTATION_ITEM ( '' )  );
#12973=DIRECTION ( 'NONE',  ( -1.111814006898795283E-16, 5.922860397471810542E-17, -1.000000000000000000 ) ) ;
#12992=ORIENTED_EDGE ( 'NONE', *, *, #14631, .F. ) ;
#12995=PLANE ( 'NONE',  #13815 ) ;
#13008=VECTOR ( 'NONE', #8517, 1000.000000000000114 ) ;
#13010=ADVANCED_FACE ( 'NONE', ( #10344 ), #4804, .F. ) ;
#13014=ORIENTED_EDGE ( 'NONE', *, *, #17649, .F. ) ;
#13039=VECTOR ( 'NONE', #17646, 1000.000000000000000 ) ;
#13044=VERTEX_POINT ( 'NONE', #13224 ) ;
#13046=CARTESIAN_POINT ( 'NONE',  ( -1.392380047608626992, 49.84925249003584469, 85.23980501161585721 ) ) ;
#13081=CARTESIAN_POINT ( 'NONE',  ( 1.119863296874943126, 50.25084051303456789, 61.06567965797611208 ) ) ;
#13088=VERTEX_POINT ( 'NONE', #16105 ) ;
#13092=EDGE_CURVE ( 'NONE', #4359, #10285, #4801, .T. ) ;
#13096=ORIENTED_EDGE ( 'NONE', *, *, #2519, .F. ) ;
#13104=CARTESIAN_POINT ( 'NONE',  ( 14.52215374030650175, 40.36218137147969287, 105.5543387995309956 ) ) ;
#13134=CARTESIAN_POINT ( 'NONE',  ( 0.5221537403065364957, 44.16218137147969003, 123.5543387995310098 ) ) ;
#13144=EDGE_CURVE ( 'NONE', #6239, #5759, #847, .T. ) ;
#13145=CARTESIAN_POINT ( 'NONE',  ( 27.27315414062681853, 40.36218137147969287, 105.5543387995310098 ) ) ;
#13147=ORIENTED_EDGE ( 'NONE', *, *, #6626, .T. ) ;
#13149=CARTESIAN_POINT ( 'NONE',  ( 14.52215374030650175, 44.16218137147969003, 105.5543387995309956 ) ) ;
#13187=AXIS2_PLACEMENT_3D ( 'NONE', #19860, #5282, #15304 ) ;
#13194=TOROIDAL_SURFACE ( 'NONE', #5017, 13.99999999999999645, 4.000000000000000000 ) ;
#13209=VECTOR ( 'NONE', #2366, 1000.000000000000000 ) ;
#13218=VERTEX_POINT ( 'NONE', #2338 ) ;
#13222=ORIENTED_EDGE ( 'NONE', *, *, #1042, .F. ) ;
#13224=CARTESIAN_POINT ( 'NONE',  ( 0.5221537403065064087, 48.16218137147969003, 74.55433879953100984 ) ) ;
#13228=CARTESIAN_POINT ( 'NONE',  ( 0.5221537403065064087, 48.16218137147969003, 105.5543387995310098 ) ) ;
#13234=CARTESIAN_POINT ( 'NONE',  ( 2.522153740306511960, 47.62628298661745418, 45.55433879953100273 ) ) ;
#13249=VERTEX_POINT ( 'NONE', #13723 ) ;
#13259=ORIENTED_EDGE ( 'NONE', *, *, #16236, .T. ) ;
#13273=EDGE_CURVE ( 'NONE', #347, #7250, #20159, .T. ) ;
#13280=CARTESIAN_POINT ( 'NONE',  ( 0.5221537403065054095, 50.16218137147969713, 83.55433879953099563 ) ) ;
#13295=DIRECTION ( 'NONE',  ( -9.598494438985367424E-18, 5.922860397471809309E-17, -1.000000000000000000 ) ) ;
#13309=FACE_OUTER_BOUND ( 'NONE', #3846, .T. ) ;
#13312=ORIENTED_EDGE ( 'NONE', *, *, #4327, .F. ) ;
#13329=LINE ( 'NONE', #5008, #10306 ) ;
#13341=CIRCLE ( 'NONE', #1473, 4.000000000000003553 ) ;
#13344=CARTESIAN_POINT ( 'NONE',  ( 2.122153740306511160, 47.82824192744436687, 61.55433879953100273 ) ) ;
#13366=ORIENTED_EDGE ( 'NONE', *, *, #18579, .T. ) ;
#13370=CARTESIAN_POINT ( 'NONE',  ( 2.350558581813037673, 49.87752504164859602, 61.32593395802448555 ) ) ;
#13377=EDGE_LOOP ( 'NONE', ( #13420, #10293, #13692, #20267 ) ) ;
#13382=ORIENTED_EDGE ( 'NONE', *, *, #12249, .T. ) ;
#13384=DIRECTION ( 'NONE',  ( 3.211742425186504723E-16, -5.922860397471811774E-17, 1.000000000000000000 ) ) ;
#13393=DIRECTION ( 'NONE',  ( -3.211742425186504723E-16, 5.922860397471811774E-17, -1.000000000000000000 ) ) ;
#13399=FACE_OUTER_BOUND ( 'NONE', #18951, .T. ) ;
#13420=ORIENTED_EDGE ( 'NONE', *, *, #19345, .T. ) ;
#13431=EDGE_LOOP ( 'NONE', ( #10822, #1916, #17641, #4199 ) ) ;
#13436=CARTESIAN_POINT ( 'NONE',  ( 2.263811127080454622, 49.90383875825364157, 69.41268141275703840 ) ) ;
#13442=ORIENTED_EDGE ( 'NONE', *, *, #20934, .T. ) ;
#13468=LINE ( 'NONE', #379, #2727 ) ;
#13469=VECTOR ( 'NONE', #13393, 1000.000000000000000 ) ;
#13479=ORIENTED_EDGE ( 'NONE', *, *, #1932, .F. ) ;
#13486=B_SPLINE_CURVE_WITH_KNOTS ( 'NONE', 3,
 ( #17631, #14652, #16258, #80 ),
 .UNSPECIFIED., .F., .F.,
 ( 4, 4 ),
 ( 0.01304472255648662232, 0.01428392225856177540 ),
 .UNSPECIFIED. ) ;
#13503=AXIS2_PLACEMENT_3D ( 'NONE', #13104, #14484, #8210 ) ;
#13515=DIRECTION ( 'NONE',  ( -1.110223024625156540E-16, -1.000000000000000000, -5.922860397471808077E-17 ) ) ;
#13518=VECTOR ( 'NONE', #11183, 1000.000000000000000 ) ;
#13522=LINE ( 'NONE', #15553, #20750 ) ;
#13524=ADVANCED_FACE ( 'NONE', ( #15890 ), #11418, .F. ) ;
#13532=DIRECTION ( 'NONE',  ( 1.779391786395883536E-16, 5.922860397471806844E-17, -1.000000000000000000 ) ) ;
#13536=DIRECTION ( 'NONE',  ( -1.000000000000000000, 1.110223024625156540E-16, -1.779391786395883043E-16 ) ) ;
#13539=ORIENTED_EDGE ( 'NONE', *, *, #12879, .F. ) ;
#13544=LINE ( 'NONE', #20232, #18811 ) ;
#13569=VECTOR ( 'NONE', #17434, 1000.000000000000000 ) ;
#13574=CARTESIAN_POINT ( 'NONE',  ( 2.436687528221644694, 49.84925249003585179, 69.23980501161587142 ) ) ;
#13580=FACE_OUTER_BOUND ( 'NONE', #15734, .T. ) ;
#13586=CARTESIAN_POINT ( 'NONE',  ( -1.077846259693497677, 49.76218137147969856, 85.55433879953100984 ) ) ;
#13587=ORIENTED_EDGE ( 'NONE', *, *, #16909, .F. ) ;
#13591=LINE ( 'NONE', #3904, #13469 ) ;
#13609=CARTESIAN_POINT ( 'NONE',  ( 24.52215374030649642, 44.16218137147969003, 105.5543387995310098 ) ) ;
#13641=( BOUNDED_CURVE ( )  B_SPLINE_CURVE ( 3, ( #5441, #771, #4055, #2160 ),
 .UNSPECIFIED., .F., .T. ) 
 B_SPLINE_CURVE_WITH_KNOTS ( ( 4, 4 ),
 ( 2.801755744135676629, 3.481429563043918485 ),
 .UNSPECIFIED. ) 
 CURVE ( )  GEOMETRIC_REPRESENTATION_ITEM ( )  RATIONAL_B_SPLINE_CURVE ( ( 1.000000000000000000, 0.9618726943880423486, 0.9618726943880423486, 1.000000000000000000 ) ) 
 REPRESENTATION_ITEM ( '' )  );
#13653=ORIENTED_EDGE ( 'NONE', *, *, #8324, .T. ) ;
#13656=EDGE_CURVE ( 'NONE', #8316, #2898, #13673, .T. ) ;
#13663=VERTEX_POINT ( 'NONE', #5292 ) ;
#13665=ORIENTED_EDGE ( 'NONE', *, *, #18419, .T. ) ;
#13673=CIRCLE ( 'NONE', #6521, 3.999999999999996447 ) ;
#13685=EDGE_CURVE ( 'NONE', #11711, #12006, #8623, .T. ) ;
#13688=VECTOR ( 'NONE', #13823, 1000.000000000000114 ) ;
#13690=AXIS2_PLACEMENT_3D ( 'NONE', #7329, #2446, #10865 ) ;
#13692=ORIENTED_EDGE ( 'NONE', *, *, #14297, .F. ) ;
#13694=ORIENTED_EDGE ( 'NONE', *, *, #14297, .T. ) ;
#13695=LINE ( 'NONE', #10634, #19360 ) ;
#13698=VERTEX_POINT ( 'NONE', #10756 ) ;
#13702=PLANE ( 'NONE',  #596 ) ;
#13703=CARTESIAN_POINT ( 'NONE',  ( -1.477846259693496922, 49.81903562097207327, 51.21119304902337888 ) ) ;
#13706=DIRECTION ( 'NONE',  ( -1.779391786395883536E-16, -5.922860397471805611E-17, 1.000000000000000000 ) ) ;
#13710=DIRECTION ( 'NONE',  ( -1.779391786395883536E-16, -5.922860397471805611E-17, 1.000000000000000000 ) ) ;
#13713=DIRECTION ( 'NONE',  ( 1.084202172485505420E-16, 1.000000000000000000, 0.000000000000000000 ) ) ;
#13723=CARTESIAN_POINT ( 'NONE',  ( -0.7268458593731772499, 40.36218137147969287, 105.5543387995310098 ) ) ;
#13753=DIRECTION ( 'NONE',  ( -3.211742425186504723E-16, 5.922860397471811774E-17, -1.000000000000000000 ) ) ;
#13761=DIRECTION ( 'NONE',  ( -1.110223024625156540E-16, -1.000000000000000000, -5.922860397471808077E-17 ) ) ;
#13769=DIRECTION ( 'NONE',  ( 1.779391786395883536E-16, 5.922860397471806844E-17, -1.000000000000000000 ) ) ;
#13776=DIRECTION ( 'NONE',  ( 1.110223024625156417E-16, 1.000000000000000000, 5.922860397471808077E-17 ) ) ;
#13786=EDGE_CURVE ( 'NONE', #13663, #4828, #4334, .T. ) ;
#13788=ADVANCED_FACE ( 'NONE', ( #11062 ), #17221, .F. ) ;
#13793=EDGE_CURVE ( 'NONE', #15854, #12698, #6293, .T. ) ;
#13800=DIRECTION ( 'NONE',  ( 3.211742425186504723E-16, -5.922860397471811774E-17, 1.000000000000000000 ) ) ;
#13815=AXIS2_PLACEMENT_3D ( 'NONE', #1828, #8313, #4994 ) ;
#13823=DIRECTION ( 'NONE',  ( -0.5773502691896219563, 0.5773502691896226224, -0.5773502691896327255 ) ) ;
#13847=CARTESIAN_POINT ( 'NONE',  ( -1.477846259693490705, 50.16218137147969713, 61.55433879953100273 ) ) ;
#13852=CARTESIAN_POINT ( 'NONE',  ( 0.5221537403065114047, 44.16218137147969713, 45.55433879953100273 ) ) ;
#13855=EDGE_CURVE ( 'NONE', #15529, #6294, #9146, .T. ) ;
#13861=DIRECTION ( 'NONE',  ( -1.779391786395883536E-16, -5.922860397471806844E-17, 1.000000000000000000 ) ) ;
#13879=PLANE ( 'NONE',  #3710 ) ;
#13896=VERTEX_POINT ( 'NONE', #12650 ) ;
#13901=ORIENTED_EDGE ( 'NONE', *, *, #10649, .T. ) ;
#13913=PLANE ( 'NONE',  #12830 ) ;
#13924=ORIENTED_EDGE ( 'NONE', *, *, #12095, .F. ) ;
#13938=VECTOR ( 'NONE', #13769, 1000.000000000000000 ) ;
#13962=CARTESIAN_POINT ( 'NONE',  ( -1.219503646467433589, 49.90383875825363447, 77.41268141275706682 ) ) ;
#13966=DIRECTION ( 'NONE',  ( -1.110223024625156540E-16, -1.000000000000000000, -5.922860397471808077E-17 ) ) ;
#13971=EDGE_LOOP ( 'NONE', ( #3134, #1729, #8387, #8110, #16299 ) ) ;
#14005=EDGE_CURVE ( 'NONE', #11406, #7250, #2802, .T. ) ;
#14013=EDGE_LOOP ( 'NONE', ( #11892, #9218, #3417, #15403, #15272 ) ) ;
#14019=EDGE_CURVE ( 'NONE', #3927, #1640, #17316, .T. ) ;
#14020=ORIENTED_EDGE ( 'NONE', *, *, #11853, .F. ) ;
#14022=DIRECTION ( 'NONE',  ( -1.110223024625156540E-16, -1.000000000000000000, -5.922860397471808077E-17 ) ) ;
#14029=DIRECTION ( 'NONE',  ( -1.110223024625156540E-16, -1.000000000000000000, -5.922860397471808077E-17 ) ) ;
#14045=DIRECTION ( 'NONE',  ( 1.084202172485505420E-16, 1.000000000000000000, 0.000000000000000000 ) ) ;
#14047=PLANE ( 'NONE',  #11246 ) ;
#14053=DIRECTION ( 'NONE',  ( -1.779391786395883783E-16, -5.922860397471806844E-17, 1.000000000000000000 ) ) ;
#14067=LINE ( 'NONE', #12684, #12795 ) ;
#14069=CARTESIAN_POINT ( 'NONE',  ( 2.522153740306492864, 49.81903562097208749, 51.21119304902340019 ) ) ;
#14072=FACE_OUTER_BOUND ( 'NONE', #20495, .T. ) ;
#14085=EDGE_CURVE ( 'NONE', #8218, #16809, #758, .T. ) ;
#14091=B_SPLINE_CURVE_WITH_KNOTS ( 'NONE', 3,
 ( #10253, #18112, #3533, #10037 ),
 .UNSPECIFIED., .F., .F.,
 ( 4, 4 ),
 ( 0.01428392225856177540, 0.01552286970674648242 ),
 .UNSPECIFIED. ) ;
#14105=ORIENTED_EDGE ( 'NONE', *, *, #20743, .T. ) ;
#14112=ORIENTED_EDGE ( 'NONE', *, *, #11853, .T. ) ;
#14126=ADVANCED_FACE ( 'NONE', ( #5593 ), #12098, .F. ) ;
#14142=DIRECTION ( 'NONE',  ( -1.110223024625156540E-16, -1.000000000000000000, -5.922860397471808077E-17 ) ) ;
#14165=CARTESIAN_POINT ( 'NONE',  ( 2.392664886727891460, 47.70104341108812918, 85.28382765310961133 ) ) ;
#14176=VERTEX_POINT ( 'NONE', #17197 ) ;
#14187=VECTOR ( 'NONE', #13295, 1000.000000000000000 ) ;
#14190=ORIENTED_EDGE ( 'NONE', *, *, #9609, .T. ) ;
#14240=ORIENTED_EDGE ( 'NONE', *, *, #5063, .F. ) ;
#14249=AXIS2_PLACEMENT_3D ( 'NONE', #6148, #16054, #16157 ) ;
#14285=EDGE_CURVE ( 'NONE', #16046, #20386, #5808, .T. ) ;
#14297=EDGE_CURVE ( 'NONE', #18556, #13698, #12929, .T. ) ;
#14336=ADVANCED_FACE ( 'NONE', ( #16381 ), #3387, .F. ) ;
#14344=VECTOR ( 'NONE', #2767, 1000.000000000000114 ) ;
#14345=DIRECTION ( 'NONE',  ( 1.000000000000000000, -1.110223024625156417E-16, -1.111814006898795283E-16 ) ) ;
#14352=DIRECTION ( 'NONE',  ( -1.779391786395883536E-16, -5.922860397471806844E-17, 1.000000000000000000 ) ) ;
#14353=EDGE_LOOP ( 'NONE', ( #15052, #19562, #9204, #12992, #5895 ) ) ;
#14368=CARTESIAN_POINT ( 'NONE',  ( 2.522153740306505743, 50.16218137147969713, 82.55433879953099563 ) ) ;
#14369=DIRECTION ( 'NONE',  ( 1.779391786395883536E-16, 5.922860397471806844E-17, -1.000000000000000000 ) ) ;
#14376=DIRECTION ( 'NONE',  ( -4.731737692062791983E-17, 0.7071067811865500152, 0.7071067811865451302 ) ) ;
#14377=SURFACE_STYLE_FILL_AREA ( #20948 ) ;
#14380=CARTESIAN_POINT ( 'NONE',  ( -1.477846259693490705, 50.16218137147969713, 58.55433879953100984 ) ) ;
#14381=VECTOR ( 'NONE', #7121, 1000.000000000000000 ) ;
#14387=DIRECTION ( 'NONE',  ( -1.110223024625156540E-16, -1.000000000000000000, -5.922860397471808077E-17 ) ) ;
#14413=DIRECTION ( 'NONE',  ( -1.779391786395883536E-16, -5.922860397471806844E-17, 1.000000000000000000 ) ) ;
#14414=DIRECTION ( 'NONE',  ( -3.211742425186504723E-16, 5.922860397471811774E-17, -1.000000000000000000 ) ) ;
#14419=ORIENTED_EDGE ( 'NONE', *, *, #18579, .F. ) ;
#14435=ORIENTED_EDGE ( 'NONE', *, *, #9229, .F. ) ;
#14441=( NAMED_UNIT ( * ) PLANE_ANGLE_UNIT ( ) SI_UNIT ( $, .RADIAN. ) );
#14454=CARTESIAN_POINT ( 'NONE',  ( 2.122153740306512937, 47.82824192744436687, 53.55433879953100273 ) ) ;
#14464=FACE_OUTER_BOUND ( 'NONE', #2620, .T. ) ;
#14466=CARTESIAN_POINT ( 'NONE',  ( -1.077846259693493458, 50.16218137147969713, 61.55433879953100273 ) ) ;
#14470=ADVANCED_FACE ( 'NONE', ( #13309 ), #10120, .T. ) ;
#14474=VERTEX_POINT ( 'NONE', #12037 ) ;
#14484=DIRECTION ( 'NONE',  ( -1.110223024625156540E-16, -1.000000000000000000, -5.922860397471808077E-17 ) ) ;
#14493=PLANE ( 'NONE',  #2027 ) ;
#14499=VERTEX_POINT ( 'NONE', #8520 ) ;
#14509=EDGE_LOOP ( 'NONE', ( #20770, #12713, #11424, #12909, #2627 ) ) ;
#14533=VECTOR ( 'NONE', #13800, 1000.000000000000000 ) ;
#14549=EDGE_CURVE ( 'NONE', #15405, #7189, #13341, .T. ) ;
#14561=EDGE_CURVE ( 'NONE', #15567, #1015, #4135, .T. ) ;
#14577=DIRECTION ( 'NONE',  ( -1.084202172485505420E-16, -1.000000000000000000, 0.000000000000000000 ) ) ;
#14579=CARTESIAN_POINT ( 'NONE',  ( 2.436687528221638033, 49.84925249003585179, 85.23980501161587142 ) ) ;
#14597=CARTESIAN_POINT ( 'NONE',  ( 0.5221537403065091842, 44.16218137147969713, 58.55433879953100984 ) ) ;
#14628=ORIENTED_EDGE ( 'NONE', *, *, #6946, .F. ) ;
#14631=EDGE_CURVE ( 'NONE', #16809, #7189, #15740, .T. ) ;
#14636=CARTESIAN_POINT ( 'NONE',  ( -1.077846259693496345, 47.82824192744436687, 77.55433879953099563 ) ) ;
#14652=CARTESIAN_POINT ( 'NONE',  ( -0.3208136495745970151, 40.36218137147969998, 46.22755528265711433 ) ) ;
#14655=VECTOR ( 'NONE', #3707, 1000.000000000000000 ) ;
#14664=VERTEX_POINT ( 'NONE', #16764 ) ;
#14665=CARTESIAN_POINT ( 'NONE',  ( -1.348357406114875312, 47.70104341108812918, 53.28382765310962554 ) ) ;
#14670=ADVANCED_FACE ( 'NONE', ( #15164 ), #20358, .T. ) ;
#14682=AXIS2_PLACEMENT_3D ( 'NONE', #7188, #2096, #10305 ) ;
#14694=DIRECTION ( 'NONE',  ( -2.909222284125557203E-16, -0.7071067811865512365, 0.7071067811865439090 ) ) ;
#14697=( BOUNDED_CURVE ( )  B_SPLINE_CURVE ( 3, ( #131, #19588, #3535, #14911 ),
 .UNSPECIFIED., .F., .F. ) 
 B_SPLINE_CURVE_WITH_KNOTS ( ( 4, 4 ),
 ( 1.230959417340772299, 1.276280841686757928 ),
 .UNSPECIFIED. ) 
 CURVE ( )  GEOMETRIC_REPRESENTATION_ITEM ( )  RATIONAL_B_SPLINE_CURVE ( ( 1.000000000000000000, 0.9998288380325437430, 0.9998288380325437430, 1.000000000000000000 ) ) 
 REPRESENTATION_ITEM ( '' )  );
#14716=AXIS2_PLACEMENT_3D ( 'NONE', #13847, #2477, #5763 ) ;
#14736=CARTESIAN_POINT ( 'NONE',  ( 2.522153740306508407, 50.16218137147969713, 66.55433879953099563 ) ) ;
#14737=ORIENTED_EDGE ( 'NONE', *, *, #3774, .T. ) ;
#14771=LINE ( 'NONE', #19451, #11806 ) ;
#14796=VERTEX_POINT ( 'NONE', #4085 ) ;
#14799=DIRECTION ( 'NONE',  ( -1.110223024625156540E-16, -1.000000000000000000, -5.922860397471808077E-17 ) ) ;
#14809=EDGE_CURVE ( 'NONE', #16100, #13896, #19475, .T. ) ;
#14812=ADVANCED_FACE ( 'NONE', ( #20572 ), #17697, .T. ) ;
#14836=ORIENTED_EDGE ( 'NONE', *, *, #12873, .T. ) ;
#14844=ORIENTED_EDGE ( 'NONE', *, *, #15312, .F. ) ;
#14869=VERTEX_POINT ( 'NONE', #2815 ) ;
#14870=PLANE ( 'NONE',  #13187 ) ;
#14871=VECTOR ( 'NONE', #18228, 1000.000000000000000 ) ;
#14873=PLANE ( 'NONE',  #15891 ) ;
#14899=ORIENTED_EDGE ( 'NONE', *, *, #17661, .F. ) ;
#14911=CARTESIAN_POINT ( 'NONE',  ( -1.219503646467430036, 49.90383875825363447, 69.41268141275705261 ) ) ;
#14918=DIRECTION ( 'NONE',  ( 1.000000000000000000, 0.000000000000000000, 0.000000000000000000 ) ) ;
#14924=DIRECTION ( 'NONE',  ( 0.5773502691896226224, 0.5773502691896224004, -0.5773502691896322814 ) ) ;
#14943=DIRECTION ( 'NONE',  ( 9.598494438985367424E-18, -5.922860397471809309E-17, 1.000000000000000000 ) ) ;
#14949=DIRECTION ( 'NONE',  ( -1.000000000000000000, 0.000000000000000000, 0.000000000000000000 ) ) ;
#14954=VECTOR ( 'NONE', #10302, 1000.000000000000000 ) ;
#14964=CIRCLE ( 'NONE', #15310, 3.999999999999996447 ) ;
#14968=ORIENTED_EDGE ( 'NONE', *, *, #1419, .T. ) ;
#14971=DIRECTION ( 'NONE',  ( -1.000000000000000000, 0.000000000000000000, 0.000000000000000000 ) ) ;
#14973=CIRCLE ( 'NONE', #4748, 3.199999999999987743 ) ;
#14975=FACE_OUTER_BOUND ( 'NONE', #10934, .T. ) ;
#14977=CARTESIAN_POINT ( 'NONE',  ( -1.477846259693491149, 49.76218137147969856, 61.55433879953100273 ) ) ;
#14986=CARTESIAN_POINT ( 'NONE',  ( -1.077846259693496123, 50.16218137147969713, 77.55433879953099563 ) ) ;
#15026=EDGE_LOOP ( 'NONE', ( #824, #17211, #8697, #13901, #2929 ) ) ;
#15034=CARTESIAN_POINT ( 'NONE',  ( 1.119863296874945791, 50.25084051303456789, 69.06567965797609077 ) ) ;
#15037=ORIENTED_EDGE ( 'NONE', *, *, #18817, .F. ) ;
#15048=CARTESIAN_POINT ( 'NONE',  ( 2.522153740306509295, 47.62628298661744708, 61.15433879953099705 ) ) ;
#15052=ORIENTED_EDGE ( 'NONE', *, *, #5739, .F. ) ;
#15088=VECTOR ( 'NONE', #14799, 1000.000000000000000 ) ;
#15120=CYLINDRICAL_SURFACE ( 'NONE', #16571, 4.000000000000000000 ) ;
#15125=LINE ( 'NONE', #535, #9209 ) ;
#15133=ORIENTED_EDGE ( 'NONE', *, *, #20137, .F. ) ;
#15135=ORIENTED_EDGE ( 'NONE', *, *, #10732, .T. ) ;
#15164=FACE_OUTER_BOUND ( 'NONE', #338, .T. ) ;
#15169=VERTEX_POINT ( 'NONE', #20117 ) ;
#15190=ORIENTED_EDGE ( 'NONE', *, *, #10100, .T. ) ;
#15191=DIRECTION ( 'NONE',  ( -1.779391786395883536E-16, -5.922860397471805611E-17, 1.000000000000000000 ) ) ;
#15228=LINE ( 'NONE', #10564, #9103 ) ;
#15236=ORIENTED_EDGE ( 'NONE', *, *, #10136, .T. ) ;
#15237=EDGE_CURVE ( 'NONE', #20138, #7199, #16077, .T. ) ;
#15247=LINE ( 'NONE', #7142, #13209 ) ;
#15264=( BOUNDED_CURVE ( )  B_SPLINE_CURVE ( 3, ( #8438, #39, #9833, #11645 ),
 .UNSPECIFIED., .F., .F. ) 
 B_SPLINE_CURVE_WITH_KNOTS ( ( 4, 4 ),
 ( 1.982313172862385731, 2.094395102393195263 ),
 .UNSPECIFIED. ) 
 CURVE ( )  GEOMETRIC_REPRESENTATION_ITEM ( )  RATIONAL_B_SPLINE_CURVE ( ( 1.000000000000000000, 0.9989534107080366709, 0.9989534107080366709, 1.000000000000000000 ) ) 
 REPRESENTATION_ITEM ( '' )  );
#15272=ORIENTED_EDGE ( 'NONE', *, *, #12249, .F. ) ;
#15286=CARTESIAN_POINT ( 'NONE',  ( 28.52215374030649642, 44.16218137147969003, 105.5543387995310098 ) ) ;
#15301=VECTOR ( 'NONE', #3438, 1000.000000000000000 ) ;
#15304=DIRECTION ( 'NONE',  ( -1.110223024625156540E-16, -1.000000000000000000, -5.922860397471808077E-17 ) ) ;
#15309=CARTESIAN_POINT ( 'NONE',  ( -1.477846259693495146, 47.62628298661744708, 58.55433879953100984 ) ) ;
#15310=AXIS2_PLACEMENT_3D ( 'NONE', #6896, #18499, #11804 ) ;
#15312=EDGE_CURVE ( 'NONE', #5547, #4359, #5620, .T. ) ;
#15314=PLANE ( 'NONE',  #7125 ) ;
#15323=DIRECTION ( 'NONE',  ( 1.084202172485505420E-16, 1.000000000000000000, 0.000000000000000000 ) ) ;
#15326=FACE_OUTER_BOUND ( 'NONE', #13431, .T. ) ;
#15329=CARTESIAN_POINT ( 'NONE',  ( 0.5221537403065096283, 50.16218137147969713, 59.55433879953099563 ) ) ;
#15334=LINE ( 'NONE', #18620, #7015 ) ;
#15337=CARTESIAN_POINT ( 'NONE',  ( -1.477846259693488706, 49.81903562097206617, 123.5543387995310098 ) ) ;
#15353=VERTEX_POINT ( 'NONE', #15561 ) ;
#15359=FACE_OUTER_BOUND ( 'NONE', #4629, .T. ) ;
#15360=VERTEX_POINT ( 'NONE', #6069 ) ;
#15364=DIRECTION ( 'NONE',  ( 1.779391786395883536E-16, 5.922860397471806844E-17, -1.000000000000000000 ) ) ;
#15373=ADVANCED_FACE ( 'NONE', ( #10890 ), #5970, .F. ) ;
#15383=VERTEX_POINT ( 'NONE', #15455 ) ;
#15390=ORIENTED_EDGE ( 'NONE', *, *, #3889, .T. ) ;
#15395=CARTESIAN_POINT ( 'NONE',  ( -0.07555581626192670042, 50.25084051303456789, 85.06567965797613340 ) ) ;
#15402=ORIENTED_EDGE ( 'NONE', *, *, #21034, .T. ) ;
#15403=ORIENTED_EDGE ( 'NONE', *, *, #810, .T. ) ;
#15405=VERTEX_POINT ( 'NONE', #17154 ) ;
#15410=ORIENTED_EDGE ( 'NONE', *, *, #9240, .T. ) ;
#15427=CARTESIAN_POINT ( 'NONE',  ( 2.522153740306506187, 49.81903562097208038, 77.15433879953100416 ) ) ;
#15435=EDGE_LOOP ( 'NONE', ( #4688, #13312, #20464, #4696, #13694 ) ) ;
#15455=CARTESIAN_POINT ( 'NONE',  ( 2.122153740306507608, 49.76218137147969856, 85.55433879953100984 ) ) ;
#15475=ORIENTED_EDGE ( 'NONE', *, *, #2496, .F. ) ;
#15508=DIRECTION ( 'NONE',  ( -1.571217453038212812E-16, -0.7071067811865525687, -0.7071067811865425767 ) ) ;
#15513=EDGE_LOOP ( 'NONE', ( #10522, #8553, #9026, #17101 ) ) ;
#15529=VERTEX_POINT ( 'NONE', #7084 ) ;
#15543=FACE_OUTER_BOUND ( 'NONE', #10049, .T. ) ;
#15549=DIRECTION ( 'NONE',  ( -1.779391786395883783E-16, -5.922860397471806844E-17, 1.000000000000000000 ) ) ;
#15553=CARTESIAN_POINT ( 'NONE',  ( 2.522153740306505298, 49.16218137147968292, 82.55433879953099563 ) ) ;
#15561=CARTESIAN_POINT ( 'NONE',  ( 2.522153740306506631, 49.16218137147969003, 74.55433879953100984 ) ) ;
#15565=CARTESIAN_POINT ( 'NONE',  ( 2.522153740306505298, 50.16218137147969713, 85.15433879953098995 ) ) ;
#15567=VERTEX_POINT ( 'NONE', #13586 ) ;
#15608=ORIENTED_EDGE ( 'NONE', *, *, #13786, .T. ) ;
#15620=DIRECTION ( 'NONE',  ( 1.779391786395883536E-16, 5.922860397471805611E-17, -1.000000000000000000 ) ) ;
#15631=VECTOR ( 'NONE', #9003, 1000.000000000000114 ) ;
#15660=CARTESIAN_POINT ( 'NONE',  ( -0.07555581626192474365, 50.25084051303456789, 53.06567965797612629 ) ) ;
#15661=EDGE_CURVE ( 'NONE', #1211, #11865, #19145, .T. ) ;
#15665=ORIENTED_EDGE ( 'NONE', *, *, #8352, .T. ) ;
#15706=VECTOR ( 'NONE', #14943, 1000.000000000000000 ) ;
#15720=AXIS2_PLACEMENT_3D ( 'NONE', #3993, #3679, #276 ) ;
#15730=ORIENTED_EDGE ( 'NONE', *, *, #630, .T. ) ;
#15734=EDGE_LOOP ( 'NONE', ( #2414, #7229, #13014, #8656 ) ) ;
#15740=CIRCLE ( 'NONE', #12674, 9.999999999999996447 ) ;
#15741=LINE ( 'NONE', #9144, #12261 ) ;
#15743=AXIS2_PLACEMENT_3D ( 'NONE', #4774, #14369, #3200 ) ;
#15746=DIRECTION ( 'NONE',  ( -1.110223024625156540E-16, -1.000000000000000000, -5.922860397471808077E-17 ) ) ;
#15748=DIRECTION ( 'NONE',  ( -4.731737692062791983E-17, 0.7071067811865500152, 0.7071067811865451302 ) ) ;
#15789=DIRECTION ( 'NONE',  ( -1.110223024625156540E-16, -1.000000000000000000, -5.922860397471808077E-17 ) ) ;
#15797=ORIENTED_EDGE ( 'NONE', *, *, #11706, .F. ) ;
#15833=LINE ( 'NONE', #20392, #9461 ) ;
#15834=( BOUNDED_CURVE ( )  B_SPLINE_CURVE ( 3, ( #10977, #15855, #19046, #12663 ),
 .UNSPECIFIED., .F., .F. ) 
 B_SPLINE_CURVE_WITH_KNOTS ( ( 4, 4 ),
 ( 1.982313172862381956, 2.094395102393196595 ),
 .UNSPECIFIED. ) 
 CURVE ( )  GEOMETRIC_REPRESENTATION_ITEM ( )  RATIONAL_B_SPLINE_CURVE ( ( 1.000000000000000000, 0.9989534107080366709, 0.9989534107080366709, 1.000000000000000000 ) ) 
 REPRESENTATION_ITEM ( '' )  );
#15847=CARTESIAN_POINT ( 'NONE',  ( -1.348357406114881529, 47.70104341108812918, 77.28382765310962554 ) ) ;
#15848=CARTESIAN_POINT ( 'NONE',  ( 29.77115333998617785, 40.36218137147969287, 105.5543387995309956 ) ) ;
#15854=VERTEX_POINT ( 'NONE', #4704 ) ;
#15855=CARTESIAN_POINT ( 'NONE',  ( -1.214884381343041664, 47.76843358786783966, 69.41730067788145675 ) ) ;
#15857=CARTESIAN_POINT ( 'NONE',  ( 2.522153740306509739, 47.62628298661744708, 58.55433879953100984 ) ) ;
#15890=FACE_OUTER_BOUND ( 'NONE', #5695, .T. ) ;
#15891=AXIS2_PLACEMENT_3D ( 'NONE', #16269, #1700, #20925 ) ;
#15896=EDGE_CURVE ( 'NONE', #18875, #1268, #11437, .T. ) ;
#15904=VECTOR ( 'NONE', #9905, 1000.000000000000000 ) ;
#15920=EDGE_CURVE ( 'NONE', #20386, #5547, #20099, .T. ) ;
#15926=PLANE ( 'NONE',  #2788 ) ;
#15929=DIRECTION ( 'NONE',  ( -1.000000000000000000, 1.110223024625156540E-16, -1.779391786395883043E-16 ) ) ;
#15938=EDGE_LOOP ( 'NONE', ( #4103, #6194, #44, #16422, #20264 ) ) ;
#15941=CARTESIAN_POINT ( 'NONE',  ( 2.263811127080450625, 49.90383875825364157, 85.41268141275705261 ) ) ;
#15946=CARTESIAN_POINT ( 'NONE',  ( -0.1709386726045586946, 50.28109722957945138, 83.67325465763076409 ) ) ;
#15963=PLANE ( 'NONE',  #12167 ) ;
#15964=AXIS2_PLACEMENT_3D ( 'NONE', #9619, #20565, #4493 ) ;
#15971=DIRECTION ( 'NONE',  ( -1.779391786395883536E-16, -5.922860397471806844E-17, 1.000000000000000000 ) ) ;
#15974=AXIS2_PLACEMENT_3D ( 'NONE', #6555, #1789, #19740 ) ;
#15976=VERTEX_POINT ( 'NONE', #9055 ) ;
#15992=CARTESIAN_POINT ( 'NONE',  ( 2.522153740306509739, 49.16218137147969003, 58.55433879953100984 ) ) ;
#15993=EDGE_CURVE ( 'NONE', #16819, #16316, #8845, .T. ) ;
#16000=CARTESIAN_POINT ( 'NONE',  ( 2.522153740306510183, 50.16218137147969713, 58.55433879953100984 ) ) ;
#16009=ADVANCED_FACE ( 'NONE', ( #15543 ), #961, .F. ) ;
#16023=EDGE_CURVE ( 'NONE', #7289, #1035, #1485, .T. ) ;
#16042=ORIENTED_EDGE ( 'NONE', *, *, #13656, .T. ) ;
#16046=VERTEX_POINT ( 'NONE', #2242 ) ;
#16051=LINE ( 'NONE', #11161, #19821 ) ;
#16054=DIRECTION ( 'NONE',  ( 1.779391786395883536E-16, 5.922860397471805611E-17, -1.000000000000000000 ) ) ;
#16062=ORIENTED_EDGE ( 'NONE', *, *, #4525, .T. ) ;
#16067=CARTESIAN_POINT ( 'NONE',  ( -1.477846259693493813, 50.16218137147969713, 74.55433879953100984 ) ) ;
#16069=DIRECTION ( 'NONE',  ( 4.142850521348543581E-16, -5.922860397471813007E-17, 1.000000000000000000 ) ) ;
#16077=CIRCLE ( 'NONE', #6888, 3.999999999999996447 ) ;
#16078=FACE_OUTER_BOUND ( 'NONE', #7714, .T. ) ;
#16099=EDGE_CURVE ( 'NONE', #4999, #18556, #4348, .T. ) ;
#16100=VERTEX_POINT ( 'NONE', #1272 ) ;
#16102=VERTEX_POINT ( 'NONE', #2969 ) ;
#16105=CARTESIAN_POINT ( 'NONE',  ( 2.522153740306505298, 49.16218137147968292, 82.55433879953099563 ) ) ;
#16117=EDGE_CURVE ( 'NONE', #18186, #15405, #6238, .T. ) ;
#16121=CARTESIAN_POINT ( 'NONE',  ( 1.855487073639845885, 49.49551470481303284, 85.82100546619767556 ) ) ;
#16153=CARTESIAN_POINT ( 'NONE',  ( 0.000000000000000000, 0.000000000000000000, 0.000000000000000000 ) ) ;
#16157=DIRECTION ( 'NONE',  ( -1.110223024625156540E-16, -1.000000000000000000, -5.922860397471808077E-17 ) ) ;
#16236=EDGE_CURVE ( 'NONE', #19441, #500, #12836, .T. ) ;
#16243=CARTESIAN_POINT ( 'NONE',  ( 2.122153740306508496, 49.76218137147969856, 77.55433879953099563 ) ) ;
#16258=CARTESIAN_POINT ( 'NONE',  ( 0.09439724277526655161, 40.36218137147969998, 46.15433879953098284 ) ) ;
#16262=CARTESIAN_POINT ( 'NONE',  ( 27.27315414062681853, 40.36218137147969287, 105.5543387995309956 ) ) ;
#16269=CARTESIAN_POINT ( 'NONE',  ( 2.522153740306509295, 50.16218137147969713, 61.55433879953100273 ) ) ;
#16271=CARTESIAN_POINT ( 'NONE',  ( 0.5221537403065008576, 44.16218137147969003, 105.5543387995310098 ) ) ;
#16282=ORIENTED_EDGE ( 'NONE', *, *, #11974, .T. ) ;
#16292=LINE ( 'NONE', #3205, #17632 ) ;
#16298=AXIS2_PLACEMENT_3D ( 'NONE', #11452, #9963, #6534 ) ;
#16299=ORIENTED_EDGE ( 'NONE', *, *, #5211, .T. ) ;
#16302=VECTOR ( 'NONE', #20475, 1000.000000000000000 ) ;
#16304=DIRECTION ( 'NONE',  ( -1.110223024625156540E-16, -1.000000000000000000, -5.922860397471808077E-17 ) ) ;
#16310=ORIENTED_EDGE ( 'NONE', *, *, #12879, .T. ) ;
#16311=VECTOR ( 'NONE', #7950, 1000.000000000000000 ) ;
#16316=VERTEX_POINT ( 'NONE', #15309 ) ;
#16349=CARTESIAN_POINT ( 'NONE',  ( 32.52215374030649286, 44.16218137147969003, 87.85433879953103542 ) ) ;
#16352=CARTESIAN_POINT ( 'NONE',  ( 0.5221537403065094063, 50.16218137147969713, 61.15433879953099705 ) ) ;
#16356=ORIENTED_EDGE ( 'NONE', *, *, #15993, .F. ) ;
#16363=CARTESIAN_POINT ( 'NONE',  ( 0.5221537403065086291, 44.16218137147969713, 61.55433879953100273 ) ) ;
#16365=DIRECTION ( 'NONE',  ( -1.000000000000000000, 1.110223024625156540E-16, -1.779391786395883043E-16 ) ) ;
#16381=FACE_OUTER_BOUND ( 'NONE', #2937, .T. ) ;
#16383=CYLINDRICAL_SURFACE ( 'NONE', #20632, 3.999999999999996447 ) ;
#16422=ORIENTED_EDGE ( 'NONE', *, *, #9620, .T. ) ;
#16435=CARTESIAN_POINT ( 'NONE',  ( -1.477846259693492481, 49.76218137147968434, 69.55433879953100984 ) ) ;
#16442=DIRECTION ( 'NONE',  ( 1.779391786395883536E-16, 5.922860397471806844E-17, -1.000000000000000000 ) ) ;
#16471=PLANE ( 'NONE',  #4724 ) ;
#16482=CARTESIAN_POINT ( 'NONE',  ( -1.219503646467431590, 49.90383875825363447, 61.41268141275705972 ) ) ;
#16483=EDGE_CURVE ( 'NONE', #10143, #13698, #9428, .T. ) ;
#16507=EDGE_CURVE ( 'NONE', #1035, #13218, #13544, .T. ) ;
#16534=CARTESIAN_POINT ( 'NONE',  ( 2.522153740306506187, 47.62628298661744708, 77.15433879953100416 ) ) ;
#16548=DIRECTION ( 'NONE',  ( -4.731737692062791983E-17, 0.7071067811865500152, 0.7071067811865451302 ) ) ;
#16567=CIRCLE ( 'NONE', #13503, 12.75100040032031501 ) ;
#16571=AXIS2_PLACEMENT_3D ( 'NONE', #528, #7010, #16920 ) ;
#16610=CARTESIAN_POINT ( 'NONE',  ( 0.5221537403065106275, 40.96218137147968719, 45.55433879953100273 ) ) ;
#16638=EDGE_CURVE ( 'NONE', #7250, #14796, #16051, .T. ) ;
#16652=DIRECTION ( 'NONE',  ( -2.267473790562806355E-16, 5.922860397471811774E-17, -1.000000000000000000 ) ) ;
#16654=LINE ( 'NONE', #13145, #15706 ) ;
#16682=DIRECTION ( 'NONE',  ( -1.000000000000000000, 0.000000000000000000, 0.000000000000000000 ) ) ;
#16690=CARTESIAN_POINT ( 'NONE',  ( -1.477846259693489372, 49.81903562097208038, 53.15433879953100416 ) ) ;
#16723=EDGE_CURVE ( 'NONE', #15169, #8316, #2848, .T. ) ;
#16726=VECTOR ( 'NONE', #17533, 1000.000000000000114 ) ;
#16764=CARTESIAN_POINT ( 'NONE',  ( 24.52215374030649642, 44.16218137147969003, 87.85433879953103542 ) ) ;
#16809=VERTEX_POINT ( 'NONE', #17601 ) ;
#16819=VERTEX_POINT ( 'NONE', #7513 ) ;
#16834=CARTESIAN_POINT ( 'NONE',  ( 2.122153740306496505, 49.76218137147968434, 69.55433879953100984 ) ) ;
#16835=VERTEX_POINT ( 'NONE', #18893 ) ;
#16840=LINE ( 'NONE', #7357, #6059 ) ;
#16844=CARTESIAN_POINT ( 'NONE',  ( 28.52215374030649642, 44.16218137147969003, 87.85433879953103542 ) ) ;
#16856=VERTEX_POINT ( 'NONE', #3030 ) ;
#16864=EDGE_CURVE ( 'NONE', #17901, #667, #18823, .T. ) ;
#16874=FACE_OUTER_BOUND ( 'NONE', #19386, .T. ) ;
#16887=ORIENTED_EDGE ( 'NONE', *, *, #5001, .T. ) ;
#16899=CARTESIAN_POINT ( 'NONE',  ( 0.5221537403065364957, 44.16218137147969003, 123.5543387995310098 ) ) ;
#16909=EDGE_CURVE ( 'NONE', #4527, #1211, #9999, .T. ) ;
#16920=DIRECTION ( 'NONE',  ( -1.000000000000000000, 0.000000000000000000, 0.000000000000000000 ) ) ;
#16926=DIRECTION ( 'NONE',  ( -1.779391786395883536E-16, -5.922860397471806844E-17, 1.000000000000000000 ) ) ;
#16944=EDGE_CURVE ( 'NONE', #1211, #2305, #4922, .T. ) ;
#16984=CIRCLE ( 'NONE', #15974, 3.999999999999996447 ) ;
#16988=CARTESIAN_POINT ( 'NONE',  ( -1.477846259693495146, 50.16218137147969713, 83.55433879953099563 ) ) ;
#17038=EDGE_CURVE ( 'NONE', #15353, #14869, #6601, .T. ) ;
#17044=EDGE_CURVE ( 'NONE', #19613, #14176, #7619, .T. ) ;
#17065=CARTESIAN_POINT ( 'NONE',  ( -1.477846259693489372, 49.81903562097208038, 53.15433879953100416 ) ) ;
#17069=EDGE_CURVE ( 'NONE', #11136, #7228, #6288, .T. ) ;
#17071=AXIS2_PLACEMENT_3D ( 'NONE', #13852, #5770, #17260 ) ;
#17073=EDGE_CURVE ( 'NONE', #16819, #4837, #20958, .T. ) ;
#17090=ORIENTED_EDGE ( 'NONE', *, *, #13273, .T. ) ;
#17101=ORIENTED_EDGE ( 'NONE', *, *, #12510, .F. ) ;
#17103=LINE ( 'NONE', #16988, #4124 ) ;
#17109=CARTESIAN_POINT ( 'NONE',  ( -1.477846259693491593, 47.62628298661744708, 53.15433879953100416 ) ) ;
#17119=ORIENTED_EDGE ( 'NONE', *, *, #16023, .F. ) ;
#17126=CARTESIAN_POINT ( 'NONE',  ( -1.077846259693492126, 49.76218137147969856, 53.55433879953100273 ) ) ;
#17130=EDGE_CURVE ( 'NONE', #3704, #7517, #3311, .T. ) ;
#17133=EDGE_LOOP ( 'NONE', ( #8551, #17300, #19396, #7120 ) ) ;
#17154=CARTESIAN_POINT ( 'NONE',  ( 32.52215374030650707, 44.16218137147969003, 105.5543387995309956 ) ) ;
#17197=CARTESIAN_POINT ( 'NONE',  ( 0.5221537403065064087, 48.16218137147969003, 58.55433879953100984 ) ) ;
#17207=PLANE ( 'NONE',  #19947 ) ;
#17211=ORIENTED_EDGE ( 'NONE', *, *, #219, .T. ) ;
#17221=PLANE ( 'NONE',  #6190 ) ;
#17232=DIRECTION ( 'NONE',  ( -1.110223024625156540E-16, -1.000000000000000000, -5.922860397471808077E-17 ) ) ;
#17236=VECTOR ( 'NONE', #12843, 1000.000000000000000 ) ;
#17259=SURFACE_SIDE_STYLE ('',( #14377 ) ) ;
#17260=DIRECTION ( 'NONE',  ( 1.084202172485505420E-16, 1.000000000000000000, 0.000000000000000000 ) ) ;
#17262=CARTESIAN_POINT ( 'NONE',  ( 2.259191861956064251, 47.76843358786783256, 85.41730067788145675 ) ) ;
#17273=CARTESIAN_POINT ( 'NONE',  ( 0.5221537403065107386, 50.16218137147969713, 53.15433879953100416 ) ) ;
#17285=CARTESIAN_POINT ( 'NONE',  ( 42.52215374030651418, 40.36218137147969287, 45.55432679953101172 ) ) ;
#17287=CARTESIAN_POINT ( 'NONE',  ( -1.077846259693493680, 47.82824192744436687, 61.55433879953100273 ) ) ;
#17300=ORIENTED_EDGE ( 'NONE', *, *, #9609, .F. ) ;
#17302=ORIENTED_EDGE ( 'NONE', *, *, #19596, .T. ) ;
#17303=CARTESIAN_POINT ( 'NONE',  ( -1.077846259693493458, 50.16218137147969713, 61.55433879953100273 ) ) ;
#17304=ADVANCED_FACE ( 'NONE', ( #3658 ), #8567, .F. ) ;
#17316=( BOUNDED_CURVE ( )  B_SPLINE_CURVE ( 3, ( #3785, #11890, #13574, #18257 ),
 .UNSPECIFIED., .F., .F. ) 
 B_SPLINE_CURVE_WITH_KNOTS ( ( 4, 4 ),
 ( 5.006904465492826084, 5.052225889838809714 ),
 .UNSPECIFIED. ) 
 CURVE ( )  GEOMETRIC_REPRESENTATION_ITEM ( )  RATIONAL_B_SPLINE_CURVE ( ( 1.000000000000000000, 0.9998288380325438540, 0.9998288380325438540, 1.000000000000000000 ) ) 
 REPRESENTATION_ITEM ( '' )  );
#17320=ORIENTED_EDGE ( 'NONE', *, *, #17130, .T. ) ;
#17325=DIRECTION ( 'NONE',  ( -1.110223024625156540E-16, -1.000000000000000000, -5.922860397471808077E-17 ) ) ;
#17340=AXIS2_PLACEMENT_3D ( 'NONE', #10954, #6340, #9673 ) ;
#17353=TOROIDAL_SURFACE ( 'NONE', #8175, 13.99999999999999645, 4.000000000000000000 ) ;
#17360=ORIENTED_EDGE ( 'NONE', *, *, #16483, .T. ) ;
#17364=CARTESIAN_POINT ( 'NONE',  ( 0.5221537403065100724, 44.16218137147969713, 53.55433879953100273 ) ) ;
#17371=CARTESIAN_POINT ( 'NONE',  ( 2.522153740306511516, 50.16218137147969713, 50.55433879953100273 ) ) ;
#17389=EDGE_LOOP ( 'NONE', ( #11123, #2136, #12624, #10451 ) ) ;
#17407=ORIENTED_EDGE ( 'NONE', *, *, #7390, .F. ) ;
#17424=ORIENTED_EDGE ( 'NONE', *, *, #16638, .F. ) ;
#17434=DIRECTION ( 'NONE',  ( 1.110223024625156540E-16, 1.000000000000000000, 5.922860397471808077E-17 ) ) ;
#17440=LINE ( 'NONE', #7864, #6844 ) ;
#17441=( BOUNDED_CURVE ( )  B_SPLINE_CURVE ( 3, ( #4042, #15660, #2666, #10568 ),
 .UNSPECIFIED., .F., .T. ) 
 B_SPLINE_CURVE_WITH_KNOTS ( ( 4, 4 ),
 ( 5.988669822071448934, 6.577700792287723530 ),
 .UNSPECIFIED. ) 
 CURVE ( )  GEOMETRIC_REPRESENTATION_ITEM ( )  RATIONAL_B_SPLINE_CURVE ( ( 1.000000000000000000, 0.9712952651971044071, 0.9712952651971044071, 1.000000000000000000 ) ) 
 REPRESENTATION_ITEM ( '' )  );
#17464=CARTESIAN_POINT ( 'NONE',  ( 28.52215374030649642, 44.16218137147969003, 87.05433879953100984 ) ) ;
#17480=FACE_OUTER_BOUND ( 'NONE', #190, .T. ) ;
#17495=EDGE_LOOP ( 'NONE', ( #1415, #11338, #17424, #11072, #14020 ) ) ;
#17516=ORIENTED_EDGE ( 'NONE', *, *, #17856, .F. ) ;
#17533=DIRECTION ( 'NONE',  ( -0.5773502691896252870, 0.5773502691896259531, -0.5773502691896259531 ) ) ;
#17565=CIRCLE ( 'NONE', #228, 15.24899959967967611 ) ;
#17568=SURFACE_STYLE_USAGE ( .BOTH. , #17259 ) ;
#17581=ORIENTED_EDGE ( 'NONE', *, *, #6139, .T. ) ;
#17601=CARTESIAN_POINT ( 'NONE',  ( 4.522153740306500858, 44.16218137147969003, 105.5543387995310098 ) ) ;
#17603=AXIS2_PLACEMENT_3D ( 'NONE', #4941, #1975, #5152 ) ;
#17631=CARTESIAN_POINT ( 'NONE',  ( -0.7268458593731683681, 40.36218137147969998, 46.35433879953098568 ) ) ;
#17632=VECTOR ( 'NONE', #10021, 999.9999999999998863 ) ;
#17641=ORIENTED_EDGE ( 'NONE', *, *, #14561, .F. ) ;
#17645=FACE_OUTER_BOUND ( 'NONE', #7136, .T. ) ;
#17646=DIRECTION ( 'NONE',  ( -1.000000000000000000, 1.110223024625156540E-16, -1.779391786395883043E-16 ) ) ;
#17649=EDGE_CURVE ( 'NONE', #3704, #13088, #13522, .T. ) ;
#17661=EDGE_CURVE ( 'NONE', #7199, #13044, #3731, .T. ) ;
#17669=DIRECTION ( 'NONE',  ( 1.779391786395883536E-16, 5.922860397471806844E-17, -1.000000000000000000 ) ) ;
#17690=PLANE ( 'NONE',  #7097 ) ;
#17695=ORIENTED_EDGE ( 'NONE', *, *, #11988, .T. ) ;
#17697=CYLINDRICAL_SURFACE ( 'NONE', #5525, 6.000000000000001776 ) ;
#17701=ORIENTED_EDGE ( 'NONE', *, *, #5060, .T. ) ;
#17707=EDGE_CURVE ( 'NONE', #13088, #2032, #11088, .T. ) ;
#17712=EDGE_CURVE ( 'NONE', #13044, #16046, #10946, .T. ) ;
#17723=ORIENTED_EDGE ( 'NONE', *, *, #9534, .T. ) ;
#17746=DIRECTION ( 'NONE',  ( 1.084202172485505420E-16, 1.000000000000000000, 0.000000000000000000 ) ) ;
#17750=FACE_OUTER_BOUND ( 'NONE', #15435, .T. ) ;
#17771=CARTESIAN_POINT ( 'NONE',  ( 0.5221537403065105165, 40.96218137147968719, 45.55433879953100273 ) ) ;
#17782=ORIENTED_EDGE ( 'NONE', *, *, #19537, .T. ) ;
#17811=PLANE ( 'NONE',  #4330 ) ;
#17816=ORIENTED_EDGE ( 'NONE', *, *, #4198, .T. ) ;
#17830=ADVANCED_FACE ( 'NONE', ( #16078 ), #20430, .T. ) ;
#17856=EDGE_CURVE ( 'NONE', #6568, #19622, #6154, .T. ) ;
#17881=CARTESIAN_POINT ( 'NONE',  ( 2.522153740306511960, 47.62628298661745418, 45.55433879953100273 ) ) ;
#17893=EDGE_LOOP ( 'NONE', ( #18659, #9102, #5272, #709, #20856 ) ) ;
#17901=VERTEX_POINT ( 'NONE', #17771 ) ;
#17906=DIRECTION ( 'NONE',  ( 3.211742425186504723E-16, -5.922860397471811774E-17, 1.000000000000000000 ) ) ;
#17909=CARTESIAN_POINT ( 'NONE',  ( 2.522153740306511072, 49.16218137147969003, 50.55433879953100273 ) ) ;
#17920=ORIENTED_EDGE ( 'NONE', *, *, #12493, .T. ) ;
#17934=FACE_OUTER_BOUND ( 'NONE', #17133, .T. ) ;
#17938=PLANE ( 'NONE',  #18948 ) ;
#17947=ADVANCED_FACE ( 'NONE', ( #1912 ), #12131, .T. ) ;
#17948=VECTOR ( 'NONE', #4273, 1000.000000000000000 ) ;
#17976=DIRECTION ( 'NONE',  ( -1.110223024625156540E-16, -1.000000000000000000, -5.922860397471808077E-17 ) ) ;
#17981=ORIENTED_EDGE ( 'NONE', *, *, #16236, .F. ) ;
#17983=CIRCLE ( 'NONE', #10198, 3.999999999999996447 ) ;
#17990=( BOUNDED_CURVE ( )  B_SPLINE_CURVE ( 3, ( #6540, #13046, #1870, #18240 ),
 .UNSPECIFIED., .F., .F. ) 
 B_SPLINE_CURVE_WITH_KNOTS ( ( 4, 4 ),
 ( 1.230959417340771189, 1.276280841686757483 ),
 .UNSPECIFIED. ) 
 CURVE ( )  GEOMETRIC_REPRESENTATION_ITEM ( )  RATIONAL_B_SPLINE_CURVE ( ( 1.000000000000000000, 0.9998288380325437430, 0.9998288380325437430, 1.000000000000000000 ) ) 
 REPRESENTATION_ITEM ( '' )  );
#17998=DIRECTION ( 'NONE',  ( 1.000000000000000000, -1.110223024625156540E-16, 1.779391786395883043E-16 ) ) ;
#18007=CARTESIAN_POINT ( 'NONE',  ( 28.52215374030649642, 44.16218137147969003, 87.05433879953100984 ) ) ;
#18014=LINE ( 'NONE', #11122, #20800 ) ;
#18015=ORIENTED_EDGE ( 'NONE', *, *, #8600, .T. ) ;
#18016=LINE ( 'NONE', #16435, #15301 ) ;
#18019=ORIENTED_EDGE ( 'NONE', *, *, #19537, .F. ) ;
#18027=CARTESIAN_POINT ( 'NONE',  ( -1.477846259693494702, 50.16218137147969713, 85.15433879953098995 ) ) ;
#18035=DIRECTION ( 'NONE',  ( -3.211742425186504723E-16, 5.922860397471811774E-17, -1.000000000000000000 ) ) ;
#18037=PRODUCT_DEFINITION_SHAPE ( 'NONE', 'NONE',  #8194 ) ;
#18051=CARTESIAN_POINT ( 'NONE',  ( 0.5221537403065112937, 44.16218137147969713, 46.35433879953098568 ) ) ;
#18060=DIRECTION ( 'NONE',  ( -1.110223024625156540E-16, -1.000000000000000000, -5.922860397471808077E-17 ) ) ;
#18068=EDGE_CURVE ( 'NONE', #10195, #3440, #1403, .T. ) ;
#18090=DIRECTION ( 'NONE',  ( 1.110223024625156540E-16, 1.000000000000000000, 5.922860397471808077E-17 ) ) ;
#18092=AXIS2_PLACEMENT_3D ( 'NONE', #775, #13753, #7473 ) ;
#18107=CARTESIAN_POINT ( 'NONE',  ( 0.5221537403065100724, 44.16218137147969713, 53.55433879953100273 ) ) ;
#18112=CARTESIAN_POINT ( 'NONE',  ( 0.9498231628969826534, 40.36218137147969998, 46.15433879953098284 ) ) ;
#18159=CYLINDRICAL_SURFACE ( 'NONE', #6110, 4.000000000000000000 ) ;
#18164=CARTESIAN_POINT ( 'NONE',  ( 2.522153740306507963, 50.16218137147969713, 69.55433879953100984 ) ) ;
#18168=LINE ( 'NONE', #14977, #11620 ) ;
#18182=DIRECTION ( 'NONE',  ( 1.110223024625156540E-16, 1.000000000000000000, 5.922860397471808077E-17 ) ) ;
#18186=VERTEX_POINT ( 'NONE', #15848 ) ;
#18202=EDGE_LOOP ( 'NONE', ( #20200, #6102, #6873, #11172 ) ) ;
#18210=ORIENTED_EDGE ( 'NONE', *, *, #13656, .F. ) ;
#18213=EDGE_CURVE ( 'NONE', #5759, #16046, #20824, .T. ) ;
#18228=DIRECTION ( 'NONE',  ( 1.110223024625156540E-16, 1.000000000000000000, 5.922860397471808077E-17 ) ) ;
#18240=CARTESIAN_POINT ( 'NONE',  ( -1.219503646467433144, 49.90383875825363447, 85.41268141275706682 ) ) ;
#18246=CARTESIAN_POINT ( 'NONE',  ( 2.263811127080455954, 49.90383875825364157, 53.41268141275705972 ) ) ;
#18257=CARTESIAN_POINT ( 'NONE',  ( 2.522153740306507519, 49.81903562097208038, 69.15433879953098995 ) ) ;
#18299=CARTESIAN_POINT ( 'NONE',  ( 1.855487073639843887, 49.49551470481303284, 53.82100546619766845 ) ) ;
#18300=ORIENTED_EDGE ( 'NONE', *, *, #5094, .T. ) ;
#18310=EDGE_LOOP ( 'NONE', ( #19199, #16310, #594, #9107, #7173 ) ) ;
#18340=DIRECTION ( 'NONE',  ( -1.779391786395883536E-16, -5.922860397471806844E-17, 1.000000000000000000 ) ) ;
#18366=AXIS2_PLACEMENT_3D ( 'NONE', #16153, #12647, #3061 ) ;
#18367=CARTESIAN_POINT ( 'NONE',  ( 2.522153740306504854, 49.81903562097208038, 85.15433879953098995 ) ) ;
#18372=ORIENTED_EDGE ( 'NONE', *, *, #3343, .T. ) ;
#18373=DIRECTION ( 'NONE',  ( 2.043266227890064411E-16, 0.7071067811865425767, -0.7071067811865524577 ) ) ;
#18384=CARTESIAN_POINT ( 'NONE',  ( 2.263811127080453733, 49.90383875825364157, 61.41268141275705972 ) ) ;
#18419=EDGE_CURVE ( 'NONE', #19622, #8316, #12936, .T. ) ;
#18424=AXIS2_PLACEMENT_3D ( 'NONE', #16271, #4655, #8075 ) ;
#18425=CARTESIAN_POINT ( 'NONE',  ( 2.522153740306507963, 47.62628298661744708, 66.55433879953099563 ) ) ;
#18432=ADVANCED_FACE ( 'NONE', ( #3350 ), #15926, .T. ) ;
#18441=LINE ( 'NONE', #13234, #20613 ) ;
#18447=CARTESIAN_POINT ( 'NONE',  ( 2.259191861956065139, 47.76843358786783966, 61.41730067788144964 ) ) ;
#18453=LINE ( 'NONE', #18557, #13938 ) ;
#18483=VERTEX_POINT ( 'NONE', #12825 ) ;
#18499=DIRECTION ( 'NONE',  ( 1.779391786395883536E-16, 5.922860397471806844E-17, -1.000000000000000000 ) ) ;
#18553=EDGE_CURVE ( 'NONE', #12696, #13249, #17440, .T. ) ;
#18556=VERTEX_POINT ( 'NONE', #17126 ) ;
#18557=CARTESIAN_POINT ( 'NONE',  ( 1.771153339986190067, 40.36218137147969998, 45.55433879953100273 ) ) ;
#18579=EDGE_CURVE ( 'NONE', #6883, #14176, #5844, .T. ) ;
#18581=ADVANCED_FACE ( 'NONE', ( #21024 ), #1895, .F. ) ;
#18582=ORIENTED_EDGE ( 'NONE', *, *, #7514, .T. ) ;
#18587=AXIS2_PLACEMENT_3D ( 'NONE', #15565, #2162, #13966 ) ;
#18588=EDGE_CURVE ( 'NONE', #6294, #6753, #19784, .T. ) ;
#18605=CARTESIAN_POINT ( 'NONE',  ( -0.8111795930268257404, 49.49551470481303284, 69.82100546619766135 ) ) ;
#18620=CARTESIAN_POINT ( 'NONE',  ( -1.477846259693490261, 47.62628298661744708, 45.55433879953100273 ) ) ;
#18625=DIRECTION ( 'NONE',  ( 1.110223024625156540E-16, 1.000000000000000000, 5.922860397471808077E-17 ) ) ;
#18629=CARTESIAN_POINT ( 'NONE',  ( 0.5221537403065114047, 44.16218137147969713, 45.55433879953100273 ) ) ;
#18634=CARTESIAN_POINT ( 'NONE',  ( -1.219503646467430036, 49.90383875825363447, 69.41268141275705261 ) ) ;
#18659=ORIENTED_EDGE ( 'NONE', *, *, #7927, .F. ) ;
#18660=CARTESIAN_POINT ( 'NONE',  ( 28.52215374030650352, 44.16218137147969003, 105.5543387995309956 ) ) ;
#18672=ORIENTED_EDGE ( 'NONE', *, *, #10710, .T. ) ;
#18677=VECTOR ( 'NONE', #18340, 1000.000000000000000 ) ;
#18688=DIRECTION ( 'NONE',  ( -1.110223024625156540E-16, -1.000000000000000000, -5.922860397471808077E-17 ) ) ;
#18716=ORIENTED_EDGE ( 'NONE', *, *, #12493, .F. ) ;
#18727=ORIENTED_EDGE ( 'NONE', *, *, #6887, .F. ) ;
#18732=CARTESIAN_POINT ( 'NONE',  ( 2.522153740306511072, 50.16218137147969713, 53.55433879953100273 ) ) ;
#18736=AXIS2_PLACEMENT_3D ( 'NONE', #3510, #4773, #14577 ) ;
#18767=VECTOR ( 'NONE', #6635, 999.9999999999998863 ) ;
#18783=CARTESIAN_POINT ( 'NONE',  ( -1.477846259693489150, 50.16218137147969713, 51.55433879953100273 ) ) ;
#18786=CARTESIAN_POINT ( 'NONE',  ( 29.36559987429793139, 40.36218137147969287, 87.72770477045767734 ) ) ;
#18797=ORIENTED_EDGE ( 'NONE', *, *, #12534, .F. ) ;
#18799=ORIENTED_EDGE ( 'NONE', *, *, #1576, .F. ) ;
#18808=( BOUNDED_CURVE ( )  B_SPLINE_CURVE ( 3, ( #20331, #12273, #4170, #10695 ),
 .UNSPECIFIED., .F., .F. ) 
 B_SPLINE_CURVE_WITH_KNOTS ( ( 4, 4 ),
 ( 2.801755744135677517, 3.481429563043919373 ),
 .UNSPECIFIED. ) 
 CURVE ( )  GEOMETRIC_REPRESENTATION_ITEM ( )  RATIONAL_B_SPLINE_CURVE ( ( 1.000000000000000000, 0.9618726943880423486, 0.9618726943880423486, 1.000000000000000000 ) ) 
 REPRESENTATION_ITEM ( '' )  );
#18811=VECTOR ( 'NONE', #13861, 1000.000000000000000 ) ;
#18817=EDGE_CURVE ( 'NONE', #10195, #1640, #18014, .T. ) ;
#18823=CIRCLE ( 'NONE', #8285, 3.200000000000009504 ) ;
#18835=DIRECTION ( 'NONE',  ( -1.110223024625156540E-16, -1.000000000000000000, -5.922860397471808077E-17 ) ) ;
#18847=CARTESIAN_POINT ( 'NONE',  ( 2.263811127080454622, 49.90383875825364157, 69.41268141275703840 ) ) ;
#18862=EDGE_CURVE ( 'NONE', #1135, #12698, #12805, .T. ) ;
#18863=LINE ( 'NONE', #2268, #17948 ) ;
#18875=VERTEX_POINT ( 'NONE', #8762 ) ;
#18883=ORIENTED_EDGE ( 'NONE', *, *, #5435, .F. ) ;
#18893=CARTESIAN_POINT ( 'NONE',  ( 2.522153740306494640, 49.81903562097208749, 75.21119304902340730 ) ) ;
#18896=CARTESIAN_POINT ( 'NONE',  ( -1.477846259693497366, 47.62628298661744708, 45.55433879953100273 ) ) ;
#18913=DIRECTION ( 'NONE',  ( 0.7071067811865479058, -3.662367542345315236E-17, -0.7071067811865472397 ) ) ;
#18939=ORIENTED_EDGE ( 'NONE', *, *, #9968, .T. ) ;
#18943=DIRECTION ( 'NONE',  ( -1.110223024625156540E-16, -1.000000000000000000, -5.922860397471808077E-17 ) ) ;
#18948=AXIS2_PLACEMENT_3D ( 'NONE', #16352, #170, #13536 ) ;
#18951=EDGE_LOOP ( 'NONE', ( #10985, #12154, #14737, #15665, #9081, #15037 ) ) ;
#18970=DIRECTION ( 'NONE',  ( -4.731737692062685363E-17, 0.7071067811865536790, 0.7071067811865414665 ) ) ;
#18971=ADVANCED_FACE ( 'NONE', ( #10374 ), #2123, .T. ) ;
#18973=ADVANCED_FACE ( 'NONE', ( #15359 ), #2579, .T. ) ;
#19007=CIRCLE ( 'NONE', #15964, 3.999999999999996447 ) ;
#19016=ADVANCED_FACE ( 'NONE', ( #877 ), #7362, .T. ) ;
#19018=VERTEX_POINT ( 'NONE', #14069 ) ;
#19046=CARTESIAN_POINT ( 'NONE',  ( -1.348357406114872203, 47.70104341108812918, 69.28382765310961133 ) ) ;
#19071=ORIENTED_EDGE ( 'NONE', *, *, #5001, .F. ) ;
#19087=EDGE_CURVE ( 'NONE', #347, #19613, #1511, .T. ) ;
#19109=VECTOR ( 'NONE', #15746, 1000.000000000000000 ) ;
#19144=ORIENTED_EDGE ( 'NONE', *, *, #5321, .T. ) ;
#19145=CIRCLE ( 'NONE', #5886, 3.999999999999996447 ) ;
#19148=DIRECTION ( 'NONE',  ( 1.000000000000000000, 0.000000000000000000, 0.000000000000000000 ) ) ;
#19166=ORIENTED_EDGE ( 'NONE', *, *, #1576, .T. ) ;
#19176=ORIENTED_EDGE ( 'NONE', *, *, #6345, .F. ) ;
#19194=DIRECTION ( 'NONE',  ( 3.211742425186504723E-16, -5.922860397471811774E-17, 1.000000000000000000 ) ) ;
#19199=ORIENTED_EDGE ( 'NONE', *, *, #4327, .T. ) ;
#19202=EDGE_LOOP ( 'NONE', ( #7942, #12612, #18799, #5432, #6015 ) ) ;
#19262=PRESENTATION_STYLE_ASSIGNMENT (( #17568 ) ) ;
#19266=DIRECTION ( 'NONE',  ( -1.111814006898795283E-16, 5.922860397471810542E-17, -1.000000000000000000 ) ) ;
#19270=VECTOR ( 'NONE', #10956, 1000.000000000000000 ) ;
#19284=CARTESIAN_POINT ( 'NONE',  ( -1.077846259693497899, 47.82824192744436687, 85.55433879953100984 ) ) ;
#19331=PLANE ( 'NONE',  #7795 ) ;
#19345=EDGE_CURVE ( 'NONE', #4999, #15976, #11824, .T. ) ;
#19360=VECTOR ( 'NONE', #4421, 1000.000000000000000 ) ;
#19381=CIRCLE ( 'NONE', #10237, 3.999999999999996447 ) ;
#19386=EDGE_LOOP ( 'NONE', ( #1514, #7508, #12595, #9806 ) ) ;
#19387=DIRECTION ( 'NONE',  ( -1.779391786395883536E-16, -5.922860397471805611E-17, 1.000000000000000000 ) ) ;
#19396=ORIENTED_EDGE ( 'NONE', *, *, #19982, .F. ) ;
#19401=FACE_OUTER_BOUND ( 'NONE', #17893, .T. ) ;
#19415=DIRECTION ( 'NONE',  ( 2.043266227890062685E-16, 0.7071067811865451302, -0.7071067811865500152 ) ) ;
#19433=CARTESIAN_POINT ( 'NONE',  ( 2.522153740306507963, 49.16218137147969003, 66.55433879953099563 ) ) ;
#19441=VERTEX_POINT ( 'NONE', #4347 ) ;
#19448=AXIS2_PLACEMENT_3D ( 'NONE', #15329, #2023, #2232 ) ;
#19451=CARTESIAN_POINT ( 'NONE',  ( -1.477846259693490705, 50.16218137147969713, 59.55433879953099563 ) ) ;
#19475=( BOUNDED_CURVE ( )  B_SPLINE_CURVE ( 3, ( #19284, #8015, #9318, #6301 ),
 .UNSPECIFIED., .F., .T. ) 
 B_SPLINE_CURVE_WITH_KNOTS ( ( 4, 4 ),
 ( 1.982313172862385509, 2.094395102393197927 ),
 .UNSPECIFIED. ) 
 CURVE ( )  GEOMETRIC_REPRESENTATION_ITEM ( )  RATIONAL_B_SPLINE_CURVE ( ( 1.000000000000000000, 0.9989534107080366709, 0.9989534107080366709, 1.000000000000000000 ) ) 
 REPRESENTATION_ITEM ( '' )  );
#19478=ORIENTED_EDGE ( 'NONE', *, *, #1275, .F. ) ;
#19488=VECTOR ( 'NONE', #17998, 1000.000000000000000 ) ;
#19500=ORIENTED_EDGE ( 'NONE', *, *, #5864, .T. ) ;
#19511=ADVANCED_FACE ( 'NONE', ( #17645 ), #7975, .F. ) ;
#19537=EDGE_CURVE ( 'NONE', #13249, #8576, #6525, .T. ) ;
#19562=ORIENTED_EDGE ( 'NONE', *, *, #12534, .T. ) ;
#19588=CARTESIAN_POINT ( 'NONE',  ( -1.392380047608626770, 49.84925249003585179, 69.23980501161585721 ) ) ;
#19596=EDGE_CURVE ( 'NONE', #8000, #16102, #2875, .T. ) ;
#19602=EDGE_LOOP ( 'NONE', ( #9935, #5809, #17407, #17981, #7631 ) ) ;
#19613=VERTEX_POINT ( 'NONE', #15857 ) ;
#19618=LINE ( 'NONE', #20031, #20037 ) ;
#19622=VERTEX_POINT ( 'NONE', #20833 ) ;
#19626=VECTOR ( 'NONE', #9243, 1000.000000000000000 ) ;
#19647=DIRECTION ( 'NONE',  ( 1.110223024625156540E-16, 1.000000000000000000, 5.922860397471808077E-17 ) ) ;
#19696=CARTESIAN_POINT ( 'NONE',  ( -0.8111795930268350663, 49.49551470481303284, 77.82100546619766135 ) ) ;
#19703=CARTESIAN_POINT ( 'NONE',  ( -1.477846259693493813, 49.81903562097207327, 77.15433879953100416 ) ) ;
#19713=LINE ( 'NONE', #1952, #9075 ) ;
#19740=DIRECTION ( 'NONE',  ( -1.084202172485505420E-16, -1.000000000000000000, 0.000000000000000000 ) ) ;
#19741=VECTOR ( 'NONE', #3943, 1000.000000000000000 ) ;
#19754=AXIS2_PLACEMENT_3D ( 'NONE', #12964, #6460, #3075 ) ;
#19759=EDGE_CURVE ( 'NONE', #6384, #20391, #6862, .T. ) ;
#19767=FACE_OUTER_BOUND ( 'NONE', #6836, .T. ) ;
#19778=VECTOR ( 'NONE', #4308, 1000.000000000000000 ) ;
#19781=AXIS2_PLACEMENT_3D ( 'NONE', #12115, #13706, #10532 ) ;
#19784=( BOUNDED_CURVE ( )  B_SPLINE_CURVE ( 3, ( #9784, #12856, #11384, #14454 ),
 .UNSPECIFIED., .F., .F. ) 
 B_SPLINE_CURVE_WITH_KNOTS ( ( 4, 4 ),
 ( 4.188790204786389637, 4.300872134317200945 ),
 .UNSPECIFIED. ) 
 CURVE ( )  GEOMETRIC_REPRESENTATION_ITEM ( )  RATIONAL_B_SPLINE_CURVE ( ( 1.000000000000000000, 0.9989534107080366709, 0.9989534107080366709, 1.000000000000000000 ) ) 
 REPRESENTATION_ITEM ( '' )  );
#19821=VECTOR ( 'NONE', #1474, 1000.000000000000000 ) ;
#19827=CARTESIAN_POINT ( 'NONE',  ( 0.5221537403065008576, 44.16218137147969003, 105.5543387995310098 ) ) ;
#19851=ADVANCED_FACE ( 'NONE', ( #12219 ), #4011, .F. ) ;
#19859=ORIENTED_EDGE ( 'NONE', *, *, #14631, .T. ) ;
#19860=CARTESIAN_POINT ( 'NONE',  ( 2.522153740306506631, 50.16218137147969713, 77.55433879953099563 ) ) ;
#19868=DIRECTION ( 'NONE',  ( -1.000000000000000000, 0.000000000000000000, 0.000000000000000000 ) ) ;
#19908=CARTESIAN_POINT ( 'NONE',  ( -1.219503646467430036, 49.90383875825363447, 69.41268141275705261 ) ) ;
#19920=MECHANICAL_DESIGN_GEOMETRIC_PRESENTATION_REPRESENTATION('',(#12472),#2957);
#19925=CARTESIAN_POINT ( 'NONE',  ( -1.477846259693498476, 49.81903562097206617, 67.21119304902336467 ) ) ;
#19947=AXIS2_PLACEMENT_3D ( 'NONE', #20598, #15620, #7414 ) ;
#19954=VERTEX_POINT ( 'NONE', #7534 ) ;
#19974=CARTESIAN_POINT ( 'NONE',  ( 0.5221537403065077410, 44.16218137147969713, 66.55433879953099563 ) ) ;
#19976=DIRECTION ( 'NONE',  ( -1.000000000000000000, 1.110223024625156540E-16, -1.779391786395883043E-16 ) ) ;
#19982=EDGE_CURVE ( 'NONE', #9317, #12054, #12952, .T. ) ;
#19989=VERTEX_POINT ( 'NONE', #15941 ) ;
#20002=ORIENTED_EDGE ( 'NONE', *, *, #16864, .T. ) ;
#20005=CIRCLE ( 'NONE', #5750, 3.200000000000009504 ) ;
#20031=CARTESIAN_POINT ( 'NONE',  ( 2.522153740306507075, 50.16218137147969713, 75.55433879953099563 ) ) ;
#20037=VECTOR ( 'NONE', #16548, 1000.000000000000114 ) ;
#20047=ORIENTED_EDGE ( 'NONE', *, *, #17856, .T. ) ;
#20088=ADVANCED_FACE ( 'NONE', ( #1252 ), #1363, .F. ) ;
#20099=LINE ( 'NONE', #12143, #14381 ) ;
#20117=CARTESIAN_POINT ( 'NONE',  ( 2.522153740306511072, 47.62628298661745418, 50.55433879953100273 ) ) ;
#20137=EDGE_CURVE ( 'NONE', #11865, #8000, #13468, .T. ) ;
#20138=VERTEX_POINT ( 'NONE', #3475 ) ;
#20151=EDGE_CURVE ( 'NONE', #7199, #500, #16984, .T. ) ;
#20159=( BOUNDED_CURVE ( )  B_SPLINE_CURVE ( 3, ( #15048, #1959, #18447, #462 ),
 .UNSPECIFIED., .F., .F. ) 
 B_SPLINE_CURVE_WITH_KNOTS ( ( 4, 4 ),
 ( 4.188790204786391413, 4.300872134317200945 ),
 .UNSPECIFIED. ) 
 CURVE ( )  GEOMETRIC_REPRESENTATION_ITEM ( )  RATIONAL_B_SPLINE_CURVE ( ( 1.000000000000000000, 0.9989534107080366709, 0.9989534107080366709, 1.000000000000000000 ) ) 
 REPRESENTATION_ITEM ( '' )  );
#20161=AXIS2_PLACEMENT_3D ( 'NONE', #9275, #16069, #19148 ) ;
#20180=DIRECTION ( 'NONE',  ( 0.5773502691896226224, 0.5773502691896224004, -0.5773502691896322814 ) ) ;
#20200=ORIENTED_EDGE ( 'NONE', *, *, #2882, .T. ) ;
#20214=CARTESIAN_POINT ( 'NONE',  ( 2.522153740306506187, 47.62628298661744708, 77.15433879953100416 ) ) ;
#20221=DIRECTION ( 'NONE',  ( 1.110223024625156540E-16, 1.000000000000000000, 5.922860397471808077E-17 ) ) ;
#20232=CARTESIAN_POINT ( 'NONE',  ( -1.477846259693495146, 47.62628298661744708, 45.55433879953100273 ) ) ;
#20264=ORIENTED_EDGE ( 'NONE', *, *, #3138, .T. ) ;
#20267=ORIENTED_EDGE ( 'NONE', *, *, #16099, .F. ) ;
#20288=EDGE_CURVE ( 'NONE', #1015, #19989, #8240, .T. ) ;
#20298=CARTESIAN_POINT ( 'NONE',  ( 2.350558581813033232, 49.87752504164860312, 77.32593395802449265 ) ) ;
#20306=ORIENTED_EDGE ( 'NONE', *, *, #15237, .T. ) ;
#20331=CARTESIAN_POINT ( 'NONE',  ( 2.522153740306494640, 49.81903562097208749, 75.21119304902340730 ) ) ;
#20336=ORIENTED_EDGE ( 'NONE', *, *, #12878, .F. ) ;
#20346=AXIS2_PLACEMENT_3D ( 'NONE', #18164, #16365, #18060 ) ;
#20355=CIRCLE ( 'NONE', #12222, 4.000000000000003553 ) ;
#20358=CYLINDRICAL_SURFACE ( 'NONE', #9283, 6.000000000000001776 ) ;
#20370=AXIS2_PLACEMENT_3D ( 'NONE', #3670, #5053, #10182 ) ;
#20386=VERTEX_POINT ( 'NONE', #4094 ) ;
#20391=VERTEX_POINT ( 'NONE', #7510 ) ;
#20392=CARTESIAN_POINT ( 'NONE',  ( -1.477846259693492037, 50.16218137147969713, 67.55433879953099563 ) ) ;
#20417=CARTESIAN_POINT ( 'NONE',  ( -1.477846259693493369, 50.16218137147969713, 75.55433879953099563 ) ) ;
#20427=FACE_OUTER_BOUND ( 'NONE', #19602, .T. ) ;
#20430=CONICAL_SURFACE ( 'NONE', #11613, 3.200000000000008171, 0.7853981633974533860 ) ;
#20447=CARTESIAN_POINT ( 'NONE',  ( 1.771153339986181408, 40.36218137147969287, 105.5543387995310098 ) ) ;
#20464=ORIENTED_EDGE ( 'NONE', *, *, #9968, .F. ) ;
#20475=DIRECTION ( 'NONE',  ( 3.211742425186504723E-16, -5.922860397471811774E-17, 1.000000000000000000 ) ) ;
#20477=ORIENTED_EDGE ( 'NONE', *, *, #6345, .T. ) ;
#20480=ORIENTED_EDGE ( 'NONE', *, *, #14285, .T. ) ;
#20492=CARTESIAN_POINT ( 'NONE',  ( 14.52215374030650175, 44.16218137147969003, 105.5543387995309956 ) ) ;
#20495=EDGE_LOOP ( 'NONE', ( #3545, #15236, #2729, #5338, #19144 ) ) ;
#20502=AXIS2_PLACEMENT_3D ( 'NONE', #5636, #7447, #14045 ) ;
#20516=VERTEX_POINT ( 'NONE', #6215 ) ;
#20531=DIRECTION ( 'NONE',  ( -1.000000000000000000, 1.110223024625156540E-16, 6.575695984913707633E-33 ) ) ;
#20536=ORIENTED_EDGE ( 'NONE', *, *, #7927, .T. ) ;
#20540=EDGE_CURVE ( 'NONE', #18483, #8749, #11939, .T. ) ;
#20552=ORIENTED_EDGE ( 'NONE', *, *, #14085, .T. ) ;
#20565=DIRECTION ( 'NONE',  ( 1.779391786395883536E-16, 5.922860397471806844E-17, -1.000000000000000000 ) ) ;
#20572=FACE_OUTER_BOUND ( 'NONE', #10835, .T. ) ;
#20597=ORIENTED_EDGE ( 'NONE', *, *, #4140, .F. ) ;
#20598=CARTESIAN_POINT ( 'NONE',  ( -1.477846259693494702, 50.16218137147969713, 85.55433879953100984 ) ) ;
#20599=LINE ( 'NONE', #2846, #16311 ) ;
#20608=CARTESIAN_POINT ( 'NONE',  ( -1.077846259693492348, 47.82824192744436687, 53.55433879953100273 ) ) ;
#20613=VECTOR ( 'NONE', #2267, 1000.000000000000000 ) ;
#20627=DIRECTION ( 'NONE',  ( -1.110223024625156540E-16, -1.000000000000000000, -5.922860397471808077E-17 ) ) ;
#20632=AXIS2_PLACEMENT_3D ( 'NONE', #20734, #11286, #4763 ) ;
#20636=CONICAL_SURFACE ( 'NONE', #3314, 3.200000000000008171, 0.7853981633974533860 ) ;
#20656=FACE_OUTER_BOUND ( 'NONE', #8488, .T. ) ;
#20658=ORIENTED_EDGE ( 'NONE', *, *, #9892, .T. ) ;
#20698=CIRCLE ( 'NONE', #12230, 3.999999999999996447 ) ;
#20701=CARTESIAN_POINT ( 'NONE',  ( -1.219503646467431590, 49.90383875825363447, 61.41268141275705972 ) ) ;
#20702=CARTESIAN_POINT ( 'NONE',  ( -1.077846259693481024, 50.16218137147969713, 69.55433879953100984 ) ) ;
#20708=AXIS2_PLACEMENT_3D ( 'NONE', #16000, #19387, #1421 ) ;
#20712=CARTESIAN_POINT ( 'NONE',  ( 2.522153740306505298, 47.62628298661744708, 82.55433879953099563 ) ) ;
#20724=DIRECTION ( 'NONE',  ( -1.111814006898795283E-16, 5.922860397471810542E-17, -1.000000000000000000 ) ) ;
#20734=CARTESIAN_POINT ( 'NONE',  ( 0.5221537403065114047, 44.16218137147969713, 45.55433879953100273 ) ) ;
#20743=EDGE_CURVE ( 'NONE', #11711, #20138, #15125, .T. ) ;
#20750=VECTOR ( 'NONE', #8858, 1000.000000000000000 ) ;
#20762=VECTOR ( 'NONE', #161, 1000.000000000000000 ) ;
#20770=ORIENTED_EDGE ( 'NONE', *, *, #3774, .F. ) ;
#20777=ADVANCED_FACE ( 'NONE', ( #1180 ), #14047, .F. ) ;
#20779=ORIENTED_EDGE ( 'NONE', *, *, #9272, .T. ) ;
#20788=ADVANCED_FACE ( 'NONE', ( #9058 ), #17353, .T. ) ;
#20800=VECTOR ( 'NONE', #17906, 1000.000000000000000 ) ;
#20817=( NAMED_UNIT ( * ) SI_UNIT ( $, .STERADIAN. ) SOLID_ANGLE_UNIT ( ) );
#20824=LINE ( 'NONE', #6152, #8219 ) ;
#20833=CARTESIAN_POINT ( 'NONE',  ( 0.5221537403065064087, 48.16218137147969003, 46.35433879953098568 ) ) ;
#20852=( NAMED_UNIT ( * ) SI_UNIT ( $, .STERADIAN. ) SOLID_ANGLE_UNIT ( ) );
#20856=ORIENTED_EDGE ( 'NONE', *, *, #13855, .F. ) ;
#20862=ORIENTED_EDGE ( 'NONE', *, *, #19087, .T. ) ;
#20881=CARTESIAN_POINT ( 'NONE',  ( 2.522153740306498193, 49.81903562097208038, 123.5543387995310098 ) ) ;
#20883=CARTESIAN_POINT ( 'NONE',  ( 28.52215374030649642, 44.16218137147969003, 87.85433879953103542 ) ) ;
#20914=LINE ( 'NONE', #12750, #13569 ) ;
#20925=DIRECTION ( 'NONE',  ( -1.110223024625156540E-16, -1.000000000000000000, -5.922860397471808077E-17 ) ) ;
#20929=CARTESIAN_POINT ( 'NONE',  ( 0.5221537403065064087, 48.16218137147969003, 53.55433879953100273 ) ) ;
#20934=EDGE_CURVE ( 'NONE', #5980, #11406, #14964, .T. ) ;
#20948=FILL_AREA_STYLE ('',( #9188 ) ) ;
#20951=( BOUNDED_CURVE ( )  B_SPLINE_CURVE ( 3, ( #10644, #4222, #12643, #20701 ),
 .UNSPECIFIED., .F., .F. ) 
 B_SPLINE_CURVE_WITH_KNOTS ( ( 4, 4 ),
 ( 1.230959417340772521, 1.276280841686757039 ),
 .UNSPECIFIED. ) 
 CURVE ( )  GEOMETRIC_REPRESENTATION_ITEM ( )  RATIONAL_B_SPLINE_CURVE ( ( 1.000000000000000000, 0.9998288380325438540, 0.9998288380325438540, 1.000000000000000000 ) ) 
 REPRESENTATION_ITEM ( '' )  );
#20958=LINE ( 'NONE', #15992, #19488 ) ;
#20960=VECTOR ( 'NONE', #653, 1000.000000000000000 ) ;
#20961=EDGE_LOOP ( 'NONE', ( #9543, #20597, #15608, #13222, #5021, #927 ) ) ;
#20977=VERTEX_POINT ( 'NONE', #20608 ) ;
#20983=DIRECTION ( 'NONE',  ( -9.598494438985368964E-18, 5.922860397471809309E-17, -1.000000000000000000 ) ) ;
#21024=FACE_OUTER_BOUND ( 'NONE', #15938, .T. ) ;
#21032=CARTESIAN_POINT ( 'NONE',  ( -1.477846259693492481, 50.16218137147969713, 66.55433879953099563 ) ) ;
#21034=EDGE_CURVE ( 'NONE', #1640, #19441, #15741, .T. ) ;
ENDSEC;
END-ISO-10303-21;
